ISO-10303-21;
HEADER;
/* Generated by software containing ST-Developer
 * from STEP Tools, Inc. (www.steptools.com) 
 */

FILE_DESCRIPTION(
/* description */ (''),
/* implementation_level */ '2;1');

FILE_NAME(
/* name */ 'Spring.step',
/* time_stamp */ '2026-10-04T16:36:43-07:00',
/* author */ (''),
/* organization */ (''),
/* preprocessor_version */ 'ST-DEVELOPER v20.2',
/* originating_system */ 'Autodesk Translation Framework v15.15.0.0',
/* authorisation */ '');

FILE_SCHEMA (('AUTOMOTIVE_DESIGN { 1 0 10303 214 3 1 1 }'));
ENDSEC;

DATA;
#10=MECHANICAL_DESIGN_GEOMETRIC_PRESENTATION_REPRESENTATION('',(#70),#33474);
#60=SHAPE_REPRESENTATION_RELATIONSHIP('SRR','None',#33500,#65);
#65=ADVANCED_BREP_SHAPE_REPRESENTATION('',(#75),#33472);
#70=STYLED_ITEM('',(#33531),#75);
#75=MANIFOLD_SOLID_BREP('Body1',#2810);
#86=B_SPLINE_SURFACE_WITH_KNOTS('',3,3,((#32554,#32555,#32556,#32557,#32558,
#32559,#32560,#32561,#32562,#32563,#32564,#32565,#32566,#32567,#32568,#32569,
#32570,#32571,#32572,#32573,#32574,#32575,#32576,#32577,#32578,#32579,#32580,
#32581,#32582,#32583,#32584,#32585,#32586,#32587,#32588,#32589,#32590,#32591,
#32592,#32593,#32594,#32595,#32596,#32597,#32598,#32599,#32600,#32601,#32602,
#32603,#32604,#32605,#32606,#32607,#32608,#32609,#32610,#32611,#32612,#32613,
#32614,#32615,#32616,#32617,#32618,#32619,#32620),(#32621,#32622,#32623,
#32624,#32625,#32626,#32627,#32628,#32629,#32630,#32631,#32632,#32633,#32634,
#32635,#32636,#32637,#32638,#32639,#32640,#32641,#32642,#32643,#32644,#32645,
#32646,#32647,#32648,#32649,#32650,#32651,#32652,#32653,#32654,#32655,#32656,
#32657,#32658,#32659,#32660,#32661,#32662,#32663,#32664,#32665,#32666,#32667,
#32668,#32669,#32670,#32671,#32672,#32673,#32674,#32675,#32676,#32677,#32678,
#32679,#32680,#32681,#32682,#32683,#32684,#32685,#32686,#32687),(#32688,
#32689,#32690,#32691,#32692,#32693,#32694,#32695,#32696,#32697,#32698,#32699,
#32700,#32701,#32702,#32703,#32704,#32705,#32706,#32707,#32708,#32709,#32710,
#32711,#32712,#32713,#32714,#32715,#32716,#32717,#32718,#32719,#32720,#32721,
#32722,#32723,#32724,#32725,#32726,#32727,#32728,#32729,#32730,#32731,#32732,
#32733,#32734,#32735,#32736,#32737,#32738,#32739,#32740,#32741,#32742,#32743,
#32744,#32745,#32746,#32747,#32748,#32749,#32750,#32751,#32752,#32753,#32754),
(#32755,#32756,#32757,#32758,#32759,#32760,#32761,#32762,#32763,#32764,
#32765,#32766,#32767,#32768,#32769,#32770,#32771,#32772,#32773,#32774,#32775,
#32776,#32777,#32778,#32779,#32780,#32781,#32782,#32783,#32784,#32785,#32786,
#32787,#32788,#32789,#32790,#32791,#32792,#32793,#32794,#32795,#32796,#32797,
#32798,#32799,#32800,#32801,#32802,#32803,#32804,#32805,#32806,#32807,#32808,
#32809,#32810,#32811,#32812,#32813,#32814,#32815,#32816,#32817,#32818,#32819,
#32820,#32821),(#32822,#32823,#32824,#32825,#32826,#32827,#32828,#32829,
#32830,#32831,#32832,#32833,#32834,#32835,#32836,#32837,#32838,#32839,#32840,
#32841,#32842,#32843,#32844,#32845,#32846,#32847,#32848,#32849,#32850,#32851,
#32852,#32853,#32854,#32855,#32856,#32857,#32858,#32859,#32860,#32861,#32862,
#32863,#32864,#32865,#32866,#32867,#32868,#32869,#32870,#32871,#32872,#32873,
#32874,#32875,#32876,#32877,#32878,#32879,#32880,#32881,#32882,#32883,#32884,
#32885,#32886,#32887,#32888),(#32889,#32890,#32891,#32892,#32893,#32894,
#32895,#32896,#32897,#32898,#32899,#32900,#32901,#32902,#32903,#32904,#32905,
#32906,#32907,#32908,#32909,#32910,#32911,#32912,#32913,#32914,#32915,#32916,
#32917,#32918,#32919,#32920,#32921,#32922,#32923,#32924,#32925,#32926,#32927,
#32928,#32929,#32930,#32931,#32932,#32933,#32934,#32935,#32936,#32937,#32938,
#32939,#32940,#32941,#32942,#32943,#32944,#32945,#32946,#32947,#32948,#32949,
#32950,#32951,#32952,#32953,#32954,#32955),(#32956,#32957,#32958,#32959,
#32960,#32961,#32962,#32963,#32964,#32965,#32966,#32967,#32968,#32969,#32970,
#32971,#32972,#32973,#32974,#32975,#32976,#32977,#32978,#32979,#32980,#32981,
#32982,#32983,#32984,#32985,#32986,#32987,#32988,#32989,#32990,#32991,#32992,
#32993,#32994,#32995,#32996,#32997,#32998,#32999,#33000,#33001,#33002,#33003,
#33004,#33005,#33006,#33007,#33008,#33009,#33010,#33011,#33012,#33013,#33014,
#33015,#33016,#33017,#33018,#33019,#33020,#33021,#33022),(#33023,#33024,
#33025,#33026,#33027,#33028,#33029,#33030,#33031,#33032,#33033,#33034,#33035,
#33036,#33037,#33038,#33039,#33040,#33041,#33042,#33043,#33044,#33045,#33046,
#33047,#33048,#33049,#33050,#33051,#33052,#33053,#33054,#33055,#33056,#33057,
#33058,#33059,#33060,#33061,#33062,#33063,#33064,#33065,#33066,#33067,#33068,
#33069,#33070,#33071,#33072,#33073,#33074,#33075,#33076,#33077,#33078,#33079,
#33080,#33081,#33082,#33083,#33084,#33085,#33086,#33087,#33088,#33089),
(#33090,#33091,#33092,#33093,#33094,#33095,#33096,#33097,#33098,#33099,
#33100,#33101,#33102,#33103,#33104,#33105,#33106,#33107,#33108,#33109,#33110,
#33111,#33112,#33113,#33114,#33115,#33116,#33117,#33118,#33119,#33120,#33121,
#33122,#33123,#33124,#33125,#33126,#33127,#33128,#33129,#33130,#33131,#33132,
#33133,#33134,#33135,#33136,#33137,#33138,#33139,#33140,#33141,#33142,#33143,
#33144,#33145,#33146,#33147,#33148,#33149,#33150,#33151,#33152,#33153,#33154,
#33155,#33156),(#33157,#33158,#33159,#33160,#33161,#33162,#33163,#33164,
#33165,#33166,#33167,#33168,#33169,#33170,#33171,#33172,#33173,#33174,#33175,
#33176,#33177,#33178,#33179,#33180,#33181,#33182,#33183,#33184,#33185,#33186,
#33187,#33188,#33189,#33190,#33191,#33192,#33193,#33194,#33195,#33196,#33197,
#33198,#33199,#33200,#33201,#33202,#33203,#33204,#33205,#33206,#33207,#33208,
#33209,#33210,#33211,#33212,#33213,#33214,#33215,#33216,#33217,#33218,#33219,
#33220,#33221,#33222,#33223)),.UNSPECIFIED.,.T.,.F.,.F.,(4,1,1,1,1,1,1,
4),(4,1,1,1,1,1,1,1,1,1,1,1,1,1,1,1,1,1,1,1,1,1,1,1,1,1,1,1,1,1,1,1,1,1,
1,1,1,1,1,1,1,1,1,1,1,1,1,1,1,1,1,1,1,1,1,1,1,1,1,1,1,1,1,1,4),(-3.14159265358979,
-2.24399475256414,-1.34639685153848,-0.448798950512828,0.448798950512828,
1.34639685153848,2.24399475256414,3.14159265358979),(0.,0.490873852123405,
0.98174770424681,1.47262155637022,1.96349540849362,2.45436926061703,2.94524311274043,
3.43611696486384,3.92699081698724,4.41786466911065,4.90873852123405,5.39961237335746,
5.89048622548086,6.38136007760427,6.87223392972767,7.36310778185108,7.85398163397448,
8.34485548609789,8.83572933822129,9.3266031903447,9.8174770424681,10.3083508945915,
10.7992247467149,11.2900985988383,11.7809724509617,12.2718463030851,12.7627201552085,
13.2535940073319,13.7444678594553,14.2353417115787,14.7262155637022,15.2170894158256,
15.707963267949,16.1988371200724,16.6897109721958,17.1805848243192,17.6714586764426,
18.162332528566,18.6532063806894,19.1440802328128,19.6349540849362,20.1258279370596,
20.616701789183,21.1075756413064,21.5984494934298,22.0893233455532,22.5801971976766,
23.0710710498,23.5619449019234,24.0528187540469,24.5436926061703,25.0345664582937,
25.5254403104171,26.0163141625405,26.5071880146639,26.9980618667873,27.4889357189107,
27.9798095710341,28.4706834231575,28.9615572752809,29.4524311274043,29.9433049795277,
30.4341788316511,30.9250526837745,31.4159265358979),.UNSPECIFIED.);
#95=PLANE('',#3126);
#96=PLANE('',#3127);
#406=FACE_OUTER_BOUND('',#529,.T.);
#407=FACE_OUTER_BOUND('',#530,.T.);
#408=FACE_OUTER_BOUND('',#531,.T.);
#529=EDGE_LOOP('',(#2539,#2540,#2541,#2542));
#530=EDGE_LOOP('',(#2543));
#531=EDGE_LOOP('',(#2544));
#885=B_SPLINE_CURVE_WITH_KNOTS('',3,(#33225,#33226,#33227,#33228,#33229,
#33230,#33231,#33232,#33233,#33234,#33235,#33236,#33237,#33238,#33239,#33240,
#33241,#33242,#33243,#33244,#33245,#33246,#33247,#33248,#33249,#33250,#33251,
#33252,#33253,#33254,#33255,#33256,#33257,#33258,#33259,#33260,#33261,#33262),
 .UNSPECIFIED.,.T.,.F.,(4,2,2,2,2,2,2,2,2,2,2,2,2,2,2,2,2,2,4),(0.,0.00206072859309695,
0.0220215556481098,0.0407099078585203,0.0625462239528445,0.0881430461322091,
0.1134648757547,0.139536921228863,0.159892801933617,0.179007909130638,0.198254802917601,
0.219009023030338,0.245767304565503,0.269399724022644,0.291540287076427,
0.310569846912954,0.326831397693072,0.344031389185084,0.345530869607548),
 .UNSPECIFIED.);
#886=B_SPLINE_CURVE_WITH_KNOTS('',3,(#33264,#33265,#33266,#33267,#33268,
#33269,#33270,#33271,#33272,#33273,#33274,#33275,#33276,#33277,#33278,#33279,
#33280,#33281,#33282,#33283,#33284,#33285,#33286,#33287,#33288,#33289,#33290,
#33291,#33292,#33293,#33294,#33295,#33296,#33297,#33298,#33299,#33300,#33301,
#33302,#33303,#33304,#33305,#33306,#33307,#33308,#33309,#33310,#33311,#33312,
#33313,#33314,#33315,#33316,#33317,#33318,#33319,#33320,#33321,#33322,#33323,
#33324,#33325,#33326,#33327,#33328,#33329,#33330),.UNSPECIFIED.,.F.,.F.,
(4,1,1,1,1,1,1,1,1,1,1,1,1,1,1,1,1,1,1,1,1,1,1,1,1,1,1,1,1,1,1,1,1,1,1,
1,1,1,1,1,1,1,1,1,1,1,1,1,1,1,1,1,1,1,1,1,1,1,1,1,1,1,1,1,4),(0.,0.490873852123405,
0.98174770424681,1.47262155637022,1.96349540849362,2.45436926061703,2.94524311274043,
3.43611696486384,3.92699081698724,4.41786466911065,4.90873852123405,5.39961237335746,
5.89048622548086,6.38136007760427,6.87223392972767,7.36310778185108,7.85398163397448,
8.34485548609789,8.83572933822129,9.3266031903447,9.8174770424681,10.3083508945915,
10.7992247467149,11.2900985988383,11.7809724509617,12.2718463030851,12.7627201552085,
13.2535940073319,13.7444678594553,14.2353417115787,14.7262155637022,15.2170894158256,
15.707963267949,16.1988371200724,16.6897109721958,17.1805848243192,17.6714586764426,
18.162332528566,18.6532063806894,19.1440802328128,19.6349540849362,20.1258279370596,
20.616701789183,21.1075756413064,21.5984494934298,22.0893233455532,22.5801971976766,
23.0710710498,23.5619449019234,24.0528187540469,24.5436926061703,25.0345664582937,
25.5254403104171,26.0163141625405,26.5071880146639,26.9980618667873,27.4889357189107,
27.9798095710341,28.4706834231575,28.9615572752809,29.4524311274043,29.9433049795277,
30.4341788316511,30.9250526837745,31.4159265358979),.UNSPECIFIED.);
#887=B_SPLINE_CURVE_WITH_KNOTS('',3,(#33331,#33332,#33333,#33334,#33335,
#33336,#33337,#33338,#33339,#33340,#33341,#33342,#33343,#33344,#33345,#33346,
#33347,#33348,#33349,#33350,#33351,#33352,#33353,#33354,#33355,#33356,#33357,
#33358,#33359,#33360,#33361,#33362,#33363,#33364,#33365,#33366,#33367,#33368),
 .UNSPECIFIED.,.T.,.F.,(4,2,2,2,2,2,2,2,2,2,2,2,2,2,2,2,2,2,4),(0.,0.00206072869877635,
0.0220215568887002,0.0407099101465702,0.0625462274814992,0.0881430511099225,
0.113464882180861,0.13953692914445,0.159892811025697,0.179007918914596,
0.19825481309114,0.219009033749323,0.245767316005896,0.269399736268268,
0.291540300209445,0.310569860803271,0.326831412241971,0.344031404416905,
0.345530884782505),.UNSPECIFIED.);
#1211=VERTEX_POINT('',#33224);
#1212=VERTEX_POINT('',#33263);
#1657=EDGE_CURVE('',#1211,#1211,#885,.T.);
#1658=EDGE_CURVE('',#1211,#1212,#886,.T.);
#1659=EDGE_CURVE('',#1212,#1212,#887,.T.);
#2539=ORIENTED_EDGE('',*,*,#1657,.T.);
#2540=ORIENTED_EDGE('',*,*,#1658,.T.);
#2541=ORIENTED_EDGE('',*,*,#1659,.F.);
#2542=ORIENTED_EDGE('',*,*,#1658,.F.);
#2543=ORIENTED_EDGE('',*,*,#1659,.T.);
#2544=ORIENTED_EDGE('',*,*,#1657,.F.);
#2793=ADVANCED_FACE('',(#406),#86,.T.);
#2794=ADVANCED_FACE('',(#407),#95,.F.);
#2795=ADVANCED_FACE('',(#408),#96,.T.);
#2810=CLOSED_SHELL('',(#2793,#2794,#2795));
#3125=AXIS2_PLACEMENT_3D('',#32553,#3751,#3752);
#3126=AXIS2_PLACEMENT_3D('',#33369,#3753,#3754);
#3127=AXIS2_PLACEMENT_3D('',#33370,#3755,#3756);
#3751=DIRECTION('axis',(0.,0.,1.));
#3752=DIRECTION('refdir',(1.,0.,0.));
#3753=DIRECTION('center_axis',(1.22464679914735E-15,1.,0.));
#3754=DIRECTION('ref_axis',(0.,0.,1.));
#3755=DIRECTION('center_axis',(0.,1.,0.));
#3756=DIRECTION('ref_axis',(0.,0.,1.));
#32553=CARTESIAN_POINT('',(0.,0.,0.));
#32554=CARTESIAN_POINT('Ctrl Pts',(-4.,0.,5.));
#32555=CARTESIAN_POINT('Ctrl Pts',(-4.05262307141051,-0.654498469497874,
5.09114583333333));
#32556=CARTESIAN_POINT('Ctrl Pts',(-3.83031081101585,-2.0164870728516,5.2734375));
#32557=CARTESIAN_POINT('Ctrl Pts',(-2.51852354898032,-3.7208214715467,5.546875));
#32558=CARTESIAN_POINT('Ctrl Pts',(-0.483385262891241,-4.63216118014149,
5.82031249999999));
#32559=CARTESIAN_POINT('Ctrl Pts',(1.8202315402997,-4.46495458019068,6.09375000000001));
#32560=CARTESIAN_POINT('Ctrl Pts',(3.83708110788313,-3.18392684763,6.36718749999999));
#32561=CARTESIAN_POINT('Ctrl Pts',(5.04610371647275,-1.03126017046504,6.640625));
#32562=CARTESIAN_POINT('Ctrl Pts',(5.09366526266359,1.51694087528755,6.9140625));
#32563=CARTESIAN_POINT('Ctrl Pts',(3.89334793428042,3.85517018194508,7.1875));
#32564=CARTESIAN_POINT('Ctrl Pts',(1.66401832874098,5.39254335225655,7.4609375));
#32565=CARTESIAN_POINT('Ctrl Pts',(-1.10655649717025,5.70140348716183,7.73437499999999));
#32566=CARTESIAN_POINT('Ctrl Pts',(-3.76778215269101,4.63360702978987,8.0078125));
#32567=CARTESIAN_POINT('Ctrl Pts',(-5.65899445677288,2.37325046891981,8.28125));
#32568=CARTESIAN_POINT('Ctrl Pts',(-6.27308950292314,-0.59072056165688,
8.5546875));
#32569=CARTESIAN_POINT('Ctrl Pts',(-5.39055984190282,-3.56939135267172,
8.828125));
#32570=CARTESIAN_POINT('Ctrl Pts',(-3.14892433147632,-5.83395881494245,
9.10156249999999));
#32571=CARTESIAN_POINT('Ctrl Pts',(-0.0269941651234124,-6.79383570767807,
9.375));
#32572=CARTESIAN_POINT('Ctrl Pts',(3.25625963494257,-6.14929751664737,9.64843749999999));
#32573=CARTESIAN_POINT('Ctrl Pts',(5.90717602022873,-3.9795144383767,9.921875));
#32574=CARTESIAN_POINT('Ctrl Pts',(7.24915357717334,-0.741104090144106,
10.1953125));
#32575=CARTESIAN_POINT('Ctrl Pts',(6.89437699385751,2.82652617704715,10.46875));
#32576=CARTESIAN_POINT('Ctrl Pts',(4.85214544364602,5.8698051725334,10.7421875));
#32577=CARTESIAN_POINT('Ctrl Pts',(1.54426647303593,7.62518428271038,11.015625));
#32578=CARTESIAN_POINT('Ctrl Pts',(-2.28027404042269,7.61004816114384,11.2890625));
#32579=CARTESIAN_POINT('Ctrl Pts',(-5.71458753487403,5.75276305414747,11.5625));
#32580=CARTESIAN_POINT('Ctrl Pts',(-7.90892381685067,2.42735464211985,11.8359375));
#32581=CARTESIAN_POINT('Ctrl Pts',(-8.280487904502,-1.61956843656331,12.109375));
#32582=CARTESIAN_POINT('Ctrl Pts',(-6.66632390115336,-5.43598980597183,
12.3828125));
#32583=CARTESIAN_POINT('Ctrl Pts',(-3.37955924042675,-8.08843859127204,
12.65625));
#32584=CARTESIAN_POINT('Ctrl Pts',(0.848467586061227,-8.89003850095873,
12.9296875));
#32585=CARTESIAN_POINT('Ctrl Pts',(5.03032510682704,-7.57700176269046,13.203125));
#32586=CARTESIAN_POINT('Ctrl Pts',(8.15306896806033,-4.38851452128152,13.4765625));
#32587=CARTESIAN_POINT('Ctrl Pts',(9.42344702515047,-0.0269941685586242,
13.75));
#32588=CARTESIAN_POINT('Ctrl Pts',(8.46840766181913,4.49584983333495,14.0234375));
#32589=CARTESIAN_POINT('Ctrl Pts',(5.44044821239548,8.09361792642082,14.296875));
#32590=CARTESIAN_POINT('Ctrl Pts',(0.998851072840637,9.86610260310719,14.5703125));
#32591=CARTESIAN_POINT('Ctrl Pts',(-3.83283486415787,9.32382107321317,14.84375));
#32592=CARTESIAN_POINT('Ctrl Pts',(-7.90252221315964,6.52035320687432,15.1171875));
#32593=CARTESIAN_POINT('Ctrl Pts',(-10.2042683613299,2.05727819272983,15.390625));
#32594=CARTESIAN_POINT('Ctrl Pts',(-10.1264293031967,-3.04360991455306,
15.6640625));
#32595=CARTESIAN_POINT('Ctrl Pts',(-7.61217905231046,-7.57400353305939,
15.9375));
#32596=CARTESIAN_POINT('Ctrl Pts',(-3.19069051639217,-10.4253049589896,
16.2109375));
#32597=CARTESIAN_POINT('Ctrl Pts',(2.13258015658974,-10.859571982884,16.484375));
#32598=CARTESIAN_POINT('Ctrl Pts',(7.10419756851087,-8.69904094228735,16.7578125));
#32599=CARTESIAN_POINT('Ctrl Pts',(10.5178826720182,-4.38586792650576,17.03125));
#32600=CARTESIAN_POINT('Ctrl Pts',(11.506987524106,1.10621456668648,17.3046875));
#32601=CARTESIAN_POINT('Ctrl Pts',(9.76344367445795,6.49125888499182,17.578125));
#32602=CARTESIAN_POINT('Ctrl Pts',(5.62810470852332,10.4721791049393,17.8515625));
#32603=CARTESIAN_POINT('Ctrl Pts',(0.0269941874218459,12.0530583592068,
18.125));
#32604=CARTESIAN_POINT('Ctrl Pts',(-5.73544006773032,10.7875177817739,18.3984375));
#32605=CARTESIAN_POINT('Ctrl Pts',(-10.2800597580419,6.90138203286673,18.671875));
#32606=CARTESIAN_POINT('Ctrl Pts',(-12.4830517794477,1.25659796463401,18.9453125));
#32607=CARTESIAN_POINT('Ctrl Pts',(-11.7532648511587,-4.83914337048452,
19.21875));
#32608=CARTESIAN_POINT('Ctrl Pts',(-8.18856157315,-9.93523961480004,19.4921875));
#32609=CARTESIAN_POINT('Ctrl Pts',(-2.57028870635813,-12.7833517182835,
19.765625));
#32610=CARTESIAN_POINT('Ctrl Pts',(3.80694337685198,-12.6428118882295,20.0390625));
#32611=CARTESIAN_POINT('Ctrl Pts',(9.43342435418766,-9.47159216503061,20.3125));
#32612=CARTESIAN_POINT('Ctrl Pts',(12.9416764567355,-3.95403216061098,20.5859375));
#32613=CARTESIAN_POINT('Ctrl Pts',(13.4386753471291,2.64560341469982,20.859375));
#32614=CARTESIAN_POINT('Ctrl Pts',(10.731719416327,8.77238225818101,21.1328125));
#32615=CARTESIAN_POINT('Ctrl Pts',(5.39225375379758,12.9473728958347,21.40625));
#32616=CARTESIAN_POINT('Ctrl Pts',(-1.36411605698682,14.1238442145743,21.6796875));
#32617=CARTESIAN_POINT('Ctrl Pts',(-7.95188025078462,11.9500710288293,21.953125));
#32618=CARTESIAN_POINT('Ctrl Pts',(-12.791953880403,6.86731330268108,22.2265625));
#32619=CARTESIAN_POINT('Ctrl Pts',(-14.0510066394079,2.30770101502388,22.4088541666667));
#32620=CARTESIAN_POINT('Ctrl Pts',(-14.1036297108185,1.72719649817133E-14,
22.5));
#32621=CARTESIAN_POINT('Ctrl Pts',(-4.,0.,4.85040034982906));
#32622=CARTESIAN_POINT('Ctrl Pts',(-4.05262307141051,-0.654721101939438,
4.94154618316239));
#32623=CARTESIAN_POINT('Ctrl Pts',(-3.83034220978403,-2.01636569876658,
5.12383784982906));
#32624=CARTESIAN_POINT('Ctrl Pts',(-2.51853054589473,-3.72090195887707,
5.39727534982905));
#32625=CARTESIAN_POINT('Ctrl Pts',(-0.483390156018607,-4.63215288184746,
5.67071284982907));
#32626=CARTESIAN_POINT('Ctrl Pts',(1.82024146317888,-4.46499056561057,5.94415034982905));
#32627=CARTESIAN_POINT('Ctrl Pts',(3.83709775979154,-3.18393342683724,6.21758784982906));
#32628=CARTESIAN_POINT('Ctrl Pts',(5.0461260345829,-1.0312683628151,6.49102534982905));
#32629=CARTESIAN_POINT('Ctrl Pts',(5.09368654153737,1.51694929147494,6.76446284982906));
#32630=CARTESIAN_POINT('Ctrl Pts',(3.89336386627578,3.85518507450177,7.03790034982906));
#32631=CARTESIAN_POINT('Ctrl Pts',(1.66402479258124,5.39256527713564,7.31133784982906));
#32632=CARTESIAN_POINT('Ctrl Pts',(-1.10656084853258,5.70142522984817,7.58477534982906));
#32633=CARTESIAN_POINT('Ctrl Pts',(-3.76779638138169,4.63362447414178,7.85821284982905));
#32634=CARTESIAN_POINT('Ctrl Pts',(-5.65901515770697,2.37325898596484,8.13165034982906));
#32635=CARTESIAN_POINT('Ctrl Pts',(-6.27311180986061,-0.590722728563154,
8.40508784982905));
#32636=CARTESIAN_POINT('Ctrl Pts',(-5.39057847567184,-3.56940381917799,
8.67852534982906));
#32637=CARTESIAN_POINT('Ctrl Pts',(-3.14893489718495,-5.83397857329016,
8.95196284982906));
#32638=CARTESIAN_POINT('Ctrl Pts',(-0.0269941647942543,-6.79385812364079,
9.22540034982906));
#32639=CARTESIAN_POINT('Ctrl Pts',(3.25627019982838,-6.14931728059803,9.49883784982906));
#32640=CARTESIAN_POINT('Ctrl Pts',(5.90719465539629,-3.97952689087694,9.77227534982905));
#32641=CARTESIAN_POINT('Ctrl Pts',(7.24917588143762,-0.741106286459191,
10.0457128498291));
#32642=CARTESIAN_POINT('Ctrl Pts',(6.89439770007539,2.82653475360122,10.3191503498291));
#32643=CARTESIAN_POINT('Ctrl Pts',(4.85215966180167,5.86982249753558,10.5925878498291));
#32644=CARTESIAN_POINT('Ctrl Pts',(1.54427084544956,7.62520626423373,10.8660253498291));
#32645=CARTESIAN_POINT('Ctrl Pts',(-2.28028054635119,7.61006960833658,11.1394628498291));
#32646=CARTESIAN_POINT('Ctrl Pts',(-5.71460338271004,5.75277890197015,11.4129003498291));
#32647=CARTESIAN_POINT('Ctrl Pts',(-7.90894526401481,2.42736114805309,11.6863378498291));
#32648=CARTESIAN_POINT('Ctrl Pts',(-8.28050988608349,-1.61957280897544,
11.9597753498291));
#32649=CARTESIAN_POINT('Ctrl Pts',(-6.66634122603885,-5.43600402413594,
12.2332128498291));
#32650=CARTESIAN_POINT('Ctrl Pts',(-3.37956781721442,-8.08845929747025,
12.5066503498291));
#32651=CARTESIAN_POINT('Ctrl Pts',(0.848469782843532,-8.89006080526373,
12.7800878498291));
#32652=CARTESIAN_POINT('Ctrl Pts',(5.03033755839293,-7.57702039777591,13.0535253498291));
#32653=CARTESIAN_POINT('Ctrl Pts',(8.15308873387941,-4.38852508633184,13.3269628498291));
#32654=CARTESIAN_POINT('Ctrl Pts',(9.42346943737693,-0.0269941685586252,
13.6004003498291));
#32655=CARTESIAN_POINT('Ctrl Pts',(8.4684274276382,4.49586039838528,13.8738378498291));
#32656=CARTESIAN_POINT('Ctrl Pts',(5.44046066396137,8.09363656150627,14.1472753498291));
#32657=CARTESIAN_POINT('Ctrl Pts',(0.998853269622947,9.86612490741219,14.4207128498291));
#32658=CARTESIAN_POINT('Ctrl Pts',(-3.83284344094555,9.32384177941138,14.6941503498291));
#32659=CARTESIAN_POINT('Ctrl Pts',(-7.90253953804511,6.52036742503844,14.9675878498291));
#32660=CARTESIAN_POINT('Ctrl Pts',(-10.2042903429114,2.05728256514196,15.2410253498291));
#32661=CARTESIAN_POINT('Ctrl Pts',(-10.1264507503608,-3.04361642048629,
15.5144628498291));
#32662=CARTESIAN_POINT('Ctrl Pts',(-7.61219490014649,-7.57401938088208,
15.7879003498291));
#32663=CARTESIAN_POINT('Ctrl Pts',(-3.19069702232067,-10.4253264061823,
16.0613378498291));
#32664=CARTESIAN_POINT('Ctrl Pts',(2.13258452900337,-10.8595939644074,16.3347753498291));
#32665=CARTESIAN_POINT('Ctrl Pts',(7.10421178666652,-8.69905826728953,16.6082128498291));
#32666=CARTESIAN_POINT('Ctrl Pts',(10.5179033782361,-4.38587650305984,16.881650349829));
#32667=CARTESIAN_POINT('Ctrl Pts',(11.5070098283703,1.10621676300158,17.1550878498291));
#32668=CARTESIAN_POINT('Ctrl Pts',(9.76346230962549,6.49127133749205,17.428525349829));
#32669=CARTESIAN_POINT('Ctrl Pts',(5.62811527340914,10.47219886889,17.7019628498291));
#32670=CARTESIAN_POINT('Ctrl Pts',(0.0269941877509962,12.0530807751695,
17.975400349829));
#32671=CARTESIAN_POINT('Ctrl Pts',(-5.73545063343893,10.7875375401217,18.2488378498291));
#32672=CARTESIAN_POINT('Ctrl Pts',(-10.280078391811,6.901394499373,18.5222753498291));
#32673=CARTESIAN_POINT('Ctrl Pts',(-12.4830740863852,1.25660013154028,18.795712849829));
#32674=CARTESIAN_POINT('Ctrl Pts',(-11.7532855520928,-4.83915188752954,
19.0691503498291));
#32675=CARTESIAN_POINT('Ctrl Pts',(-8.18857580184066,-9.93525705915197,
19.342587849829));
#32676=CARTESIAN_POINT('Ctrl Pts',(-2.57029305772047,-12.7833734609698,
19.6160253498291));
#32677=CARTESIAN_POINT('Ctrl Pts',(3.80694984069224,-12.6428338131086,19.889462849829));
#32678=CARTESIAN_POINT('Ctrl Pts',(9.43344028618301,-9.4716070575873,20.1629003498291));
#32679=CARTESIAN_POINT('Ctrl Pts',(12.9416977356093,-3.95404057679838,20.4363378498291));
#32680=CARTESIAN_POINT('Ctrl Pts',(13.4386976652392,2.64561160704987,20.7097753498291));
#32681=CARTESIAN_POINT('Ctrl Pts',(10.7317360682354,8.77238883738826,20.9832128498291));
#32682=CARTESIAN_POINT('Ctrl Pts',(5.39226367667676,12.9474088812546,21.2566503498291));
#32683=CARTESIAN_POINT('Ctrl Pts',(-1.36412095011418,14.1238359162802,21.5300878498291));
#32684=CARTESIAN_POINT('Ctrl Pts',(-7.95188724769903,11.9501515161596,21.8035253498291));
#32685=CARTESIAN_POINT('Ctrl Pts',(-12.7919852791712,6.86719192859605,22.0769628498291));
#32686=CARTESIAN_POINT('Ctrl Pts',(-14.0510066394079,2.30792364746544,22.2592545164957));
#32687=CARTESIAN_POINT('Ctrl Pts',(-14.1036297108185,1.72719649817133E-14,
22.3504003498291));
#32688=CARTESIAN_POINT('Ctrl Pts',(-3.85687988625421,0.,4.552272366273));
#32689=CARTESIAN_POINT('Ctrl Pts',(-3.90950295766472,-0.631009216832047,
4.64341819960633));
#32690=CARTESIAN_POINT('Ctrl Pts',(-3.69889172862669,-1.94629413136597,
4.825709866273));
#32691=CARTESIAN_POINT('Ctrl Pts',(-2.43574645059125,-3.59690784386268,
5.099147366273));
#32692=CARTESIAN_POINT('Ctrl Pts',(-0.468778083864464,-4.48388629988577,
5.372584866273));
#32693=CARTESIAN_POINT('Ctrl Pts',(1.76320931622579,-4.32728810641048,5.646022366273));
#32694=CARTESIAN_POINT('Ctrl Pts',(3.72190061988142,-3.08940290516982,5.91945986627299));
#32695=CARTESIAN_POINT('Ctrl Pts',(4.89996324172001,-1.00218972289062,6.19289736627299));
#32696=CARTESIAN_POINT('Ctrl Pts',(4.95107819396225,1.47368683855714,6.466334866273));
#32697=CARTESIAN_POINT('Ctrl Pts',(3.78798665921667,3.7498093182653,6.73977236627299));
#32698=CARTESIAN_POINT('Ctrl Pts',(1.62076500665406,5.24995596983545,7.013209866273));
#32699=CARTESIAN_POINT('Ctrl Pts',(-1.07748742465841,5.55526338525199,7.28664736627299));
#32700=CARTESIAN_POINT('Ctrl Pts',(-3.67325548745206,4.51842592346714,7.560084866273));
#32701=CARTESIAN_POINT('Ctrl Pts',(-5.52133341543936,2.31622941794741,7.833522366273));
#32702=CARTESIAN_POINT('Ctrl Pts',(-6.12480374971085,-0.576115700560577,
8.10695986627299));
#32703=CARTESIAN_POINT('Ctrl Pts',(-5.26666817492343,-3.48660958131966,
8.380397366273));
#32704=CARTESIAN_POINT('Ctrl Pts',(-3.07868468871711,-5.70254968975686,
8.65383486627299));
#32705=CARTESIAN_POINT('Ctrl Pts',(-0.0269941654050771,-6.64483246405232,
8.92727236627299));
#32706=CARTESIAN_POINT('Ctrl Pts',(3.18601999288746,-6.0178883894713,9.20070986627299));
#32707=CARTESIAN_POINT('Ctrl Pts',(5.7832843520526,-3.89673267200036,9.47414736627299));
#32708=CARTESIAN_POINT('Ctrl Pts',(7.10086782624852,-0.726499218600172,
9.74758486627298));
#32709=CARTESIAN_POINT('Ctrl Pts',(6.75671594800256,2.76950510493386,10.021022366273));
#32710=CARTESIAN_POINT('Ctrl Pts',(4.7576187874221,5.75462410861027,10.294459866273));
#32711=CARTESIAN_POINT('Ctrl Pts',(1.51519738251008,7.47904409595247,10.567897366273));
#32712=CARTESIAN_POINT('Ctrl Pts',(-2.23702068232002,7.46746094842322,10.841334866273));
#32713=CARTESIAN_POINT('Ctrl Pts',(-5.60922633182713,5.64740185110466,11.114772366273));
#32714=CARTESIAN_POINT('Ctrl Pts',(-7.76633660413988,2.38410128401679,11.388209866273));
#32715=CARTESIAN_POINT('Ctrl Pts',(-8.13434771772362,-1.59049934604057,
11.661647366273));
#32716=CARTESIAN_POINT('Ctrl Pts',(-6.5511428372716,-5.34146314973975,11.935084866273));
#32717=CARTESIAN_POINT('Ctrl Pts',(-3.32253816823053,-7.95077754543437,
12.208522366273));
#32718=CARTESIAN_POINT('Ctrl Pts',(0.833862714351334,-8.74175274999886,
12.481959866273));
#32719=CARTESIAN_POINT('Ctrl Pts',(4.94754334078261,-7.45311009458468,12.755397366273));
#32720=CARTESIAN_POINT('Ctrl Pts',(8.0216598402205,-4.31827487908557,13.028834866273));
#32721=CARTESIAN_POINT('Ctrl Pts',(9.27444378285203,-0.0269941685586267,
13.302272366273));
#32722=CARTESIAN_POINT('Ctrl Pts',(8.3369985339793,4.42561019113901,13.575709866273));
#32723=CARTESIAN_POINT('Ctrl Pts',(5.35766644635105,7.96972625831503,13.849147366273));
#32724=CARTESIAN_POINT('Ctrl Pts',(0.98424620113075,9.71781685214733,14.122584866273));
#32725=CARTESIAN_POINT('Ctrl Pts',(-3.77581379196166,9.1861600273755,14.396022366273));
#32726=CARTESIAN_POINT('Ctrl Pts',(-7.78734114927787,6.42582655064225,14.669459866273));
#32727=CARTESIAN_POINT('Ctrl Pts',(-10.0581281745515,2.02820910220709,14.942897366273));
#32728=CARTESIAN_POINT('Ctrl Pts',(-9.98384209048586,-3.00035655645,15.216334866273));
#32729=CARTESIAN_POINT('Ctrl Pts',(-7.50681784926357,-7.46864233001658,
15.489772366273));
#32730=CARTESIAN_POINT('Ctrl Pts',(-3.1474371582895,-10.282717746269,15.763209866273));
#32731=CARTESIAN_POINT('Ctrl Pts',(2.10351106606389,-10.7134317961261,16.036647366273));
#32732=CARTESIAN_POINT('Ctrl Pts',(7.00967091228695,-8.58385987836422,16.310084866273));
#32733=CARTESIAN_POINT('Ctrl Pts',(10.3802216261632,-4.32884685439248,16.583522366273));
#32734=CARTESIAN_POINT('Ctrl Pts',(11.3587017731812,1.09160969514256,16.856959866273));
#32735=CARTESIAN_POINT('Ctrl Pts',(9.63955200628181,6.40847711861546,17.130397366273));
#32736=CARTESIAN_POINT('Ctrl Pts',(5.55786506646821,10.3407699777633,17.403834866273));
#32737=CARTESIAN_POINT('Ctrl Pts',(0.0269941871401723,11.904055115581,17.677272366273));
#32738=CARTESIAN_POINT('Ctrl Pts',(-5.66520042497109,10.6561086565884,17.950709866273));
#32739=CARTESIAN_POINT('Ctrl Pts',(-10.1561680910626,6.81860026151465,18.224147366273));
#32740=CARTESIAN_POINT('Ctrl Pts',(-12.3347660262354,1.24199310353771,18.497584866273));
#32741=CARTESIAN_POINT('Ctrl Pts',(-11.6156038098252,-4.78212231951214,
18.771022366273));
#32742=CARTESIAN_POINT('Ctrl Pts',(-8.09403490791103,-9.82005850847731,
19.044459866273));
#32743=CARTESIAN_POINT('Ctrl Pts',(-2.5412196338463,-12.6372116163736,19.317897366273));
#32744=CARTESIAN_POINT('Ctrl Pts',(3.76369005476507,-12.5002245058084,19.591334866273));
#32745=CARTESIAN_POINT('Ctrl Pts',(9.3280630791239,-9.36623130135084,19.864772366273));
#32746=CARTESIAN_POINT('Ctrl Pts',(12.7990893880342,-3.91077812388057,20.138209866273));
#32747=CARTESIAN_POINT('Ctrl Pts',(13.2925348723763,2.6165329671254,20.411647366273));
#32748=CARTESIAN_POINT('Ctrl Pts',(10.6165389283253,8.67785831572082,20.685084866273));
#32749=CARTESIAN_POINT('Ctrl Pts',(5.33523152972366,12.8097064220545,20.958522366273));
#32750=CARTESIAN_POINT('Ctrl Pts',(-1.34950887796003,13.9755693343185,21.231959866273));
#32751=CARTESIAN_POINT('Ctrl Pts',(-7.86910315239555,11.8261574011453,21.505397366273));
#32752=CARTESIAN_POINT('Ctrl Pts',(-12.6605347980139,6.79712036119543,21.778834866273));
#32753=CARTESIAN_POINT('Ctrl Pts',(-13.9078865256621,2.28421176235806,21.9611265329396));
#32754=CARTESIAN_POINT('Ctrl Pts',(-13.9605095970727,1.70966933925209E-14,
22.052272366273));
#32755=CARTESIAN_POINT('Ctrl Pts',(-3.37285122334358,0.,4.44236151564151));
#32756=CARTESIAN_POINT('Ctrl Pts',(-3.42547429475409,-0.551880177973973,
4.53350734897485));
#32757=CARTESIAN_POINT('Ctrl Pts',(-3.25447952827565,-1.70873378422384,
4.71579901564151));
#32758=CARTESIAN_POINT('Ctrl Pts',(-2.15580613893563,-3.17794748381105,
4.98923651564151));
#32759=CARTESIAN_POINT('Ctrl Pts',(-0.419383803872583,-3.98241275177538,
5.26267401564151));
#32760=CARTESIAN_POINT('Ctrl Pts',(1.57037543627681,-3.86175379164219,5.53611151564151));
#32761=CARTESIAN_POINT('Ctrl Pts',(3.33238633949545,-2.76973447564646,5.80954901564151));
#32762=CARTESIAN_POINT('Ctrl Pts',(4.40575097261005,-0.903885637798203,
6.08298651564152));
#32763=CARTESIAN_POINT('Ctrl Pts',(4.46888200381864,1.32741452063332,6.35642401564151));
#32764=CARTESIAN_POINT('Ctrl Pts',(3.43167970686377,3.39350230505294,6.62986151564152));
#32765=CARTESIAN_POINT('Ctrl Pts',(1.47449237810634,4.76775962120238,6.90329901564151));
#32766=CARTESIAN_POINT('Ctrl Pts',(-0.979182623933988,5.06105157319051,
7.17673651564152));
#32767=CARTESIAN_POINT('Ctrl Pts',(-3.35358853628449,4.12891065901958,7.45017401564151));
#32768=CARTESIAN_POINT('Ctrl Pts',(-5.05579611984973,2.12339754137519,7.72361151564152));
#32769=CARTESIAN_POINT('Ctrl Pts',(-5.62333618663063,-0.52672545107936,
7.99704901564151));
#32770=CARTESIAN_POINT('Ctrl Pts',(-4.84769567278908,-3.20666110712353,
8.27048651564151));
#32771=CARTESIAN_POINT('Ctrl Pts',(-2.84115072577757,-5.25815490214821,
8.54392401564152));
#32772=CARTESIAN_POINT('Ctrl Pts',(-0.026994165897813,-6.14093851856364,
8.81736151564151));
#32773=CARTESIAN_POINT('Ctrl Pts',(2.94848603117964,-5.57349360295854,9.09079901564151));
#32774=CARTESIAN_POINT('Ctrl Pts',(5.36431184782471,-3.6167841950648,9.36423651564152));
#32775=CARTESIAN_POINT('Ctrl Pts',(6.59940026716997,-0.677108974870978,
9.63767401564151));
#32776=CARTESIAN_POINT('Ctrl Pts',(6.29117864450327,2.57667324000092,9.91111151564152));
#32777=CARTESIAN_POINT('Ctrl Pts',(4.43795185202518,5.36510882081929,10.1845490156415));
#32778=CARTESIAN_POINT('Ctrl Pts',(1.41689255027245,6.98483233060473,10.4579865156415));
#32779=CARTESIAN_POINT('Ctrl Pts',(-2.09074799076738,6.98526450636028,10.7314240156415));
#32780=CARTESIAN_POINT('Ctrl Pts',(-5.25291950545845,5.29109502473119,11.0048615156415));
#32781=CARTESIAN_POINT('Ctrl Pts',(-7.28414016207024,2.23782859246943,11.2782990156415));
#32782=CARTESIAN_POINT('Ctrl Pts',(-7.64013595238779,-1.49219451381135,
11.5517365156415));
#32783=CARTESIAN_POINT('Ctrl Pts',(-6.16162754945752,-5.02179621432706,
11.8251740156415));
#32784=CARTESIAN_POINT('Ctrl Pts',(-3.12970630334341,-7.48524024196608,
12.0986115156415));
#32785=CARTESIAN_POINT('Ctrl Pts',(0.784472470713589,-8.2402851908586,12.3720490156415));
#32786=CARTESIAN_POINT('Ctrl Pts',(4.66759486366428,-7.03413759048006,12.6454865156415));
#32787=CARTESIAN_POINT('Ctrl Pts',(7.57726505407319,-4.08074091713133,12.9189240156415));
#32788=CARTESIAN_POINT('Ctrl Pts',(8.77054983663259,-0.0269941685586301,
13.1923615156415));
#32789=CARTESIAN_POINT('Ctrl Pts',(7.89260374783199,4.18807622918479,13.4657990156415));
#32790=CARTESIAN_POINT('Ctrl Pts',(5.07771796923272,7.55075375421039,13.7392365156415));
#32791=CARTESIAN_POINT('Ctrl Pts',(0.934855957493001,9.21634929300708,14.0126740156415));
#32792=CARTESIAN_POINT('Ctrl Pts',(-3.58298192707453,8.72062272390719,14.2861115156415));
#32793=CARTESIAN_POINT('Ctrl Pts',(-7.3978258614638,6.10615961522957,14.5595490156415));
#32794=CARTESIAN_POINT('Ctrl Pts',(-9.5639164092157,1.92990426997787,14.8329865156415));
#32795=CARTESIAN_POINT('Ctrl Pts',(-9.50164564841623,-2.85408386490263,
15.1064240156415));
#32796=CARTESIAN_POINT('Ctrl Pts',(-7.15051102289489,-7.11233550364311,
15.3798615156415));
#32797=CARTESIAN_POINT('Ctrl Pts',(-3.00116446673686,-9.800521304206,15.6532990156415));
#32798=CARTESIAN_POINT('Ctrl Pts',(2.00520623382626,-10.2192200307783,15.9267365156415));
#32799=CARTESIAN_POINT('Ctrl Pts',(6.69000397689003,-8.19434459057323,16.2001740156415));
#32800=CARTESIAN_POINT('Ctrl Pts',(9.91468432266393,-4.13601498945954,16.4736115156415));
#32801=CARTESIAN_POINT('Ctrl Pts',(10.8572342141026,1.04221945141336,16.7470490156415));
#32802=CARTESIAN_POINT('Ctrl Pts',(9.22057950205391,6.12852864167992,17.0204865156415));
#32803=CARTESIAN_POINT('Ctrl Pts',(5.3203311047604,9.8963751912505,17.2939240156415));
#32804=CARTESIAN_POINT('Ctrl Pts',(0.0269941866474298,11.4001611700923,
17.5673615156415));
#32805=CARTESIAN_POINT('Ctrl Pts',(-5.42766646203154,10.2117138689797,17.8407990156415));
#32806=CARTESIAN_POINT('Ctrl Pts',(-9.73719558892825,6.53865178731853,18.1142365156415));
#32807=CARTESIAN_POINT('Ctrl Pts',(-11.8332984631552,1.19260285405648,18.3876740156415));
#32808=CARTESIAN_POINT('Ctrl Pts',(-11.1500665142356,-4.5892904429399,18.6611115156415));
#32809=CARTESIAN_POINT('Ctrl Pts',(-7.77436795674347,-9.43054324402977,
18.9345490156415));
#32810=CARTESIAN_POINT('Ctrl Pts',(-2.44291483312187,-12.1429998043121,
19.2079865156415));
#32811=CARTESIAN_POINT('Ctrl Pts',(3.61741742621734,-12.0180281571754,19.4814240156415));
#32812=CARTESIAN_POINT('Ctrl Pts',(8.97175612677101,-9.00992428813846,19.7548615156415));
#32813=CARTESIAN_POINT('Ctrl Pts',(12.3168931978906,-3.76450580595676,20.0282990156415));
#32814=CARTESIAN_POINT('Ctrl Pts',(12.7983226032663,2.51822888203298,20.3017365156415));
#32815=CARTESIAN_POINT('Ctrl Pts',(10.2270246479393,8.35818988619747,20.5751740156415));
#32816=CARTESIAN_POINT('Ctrl Pts',(5.14239764977468,12.3441721072862,20.8486115156415));
#32817=CARTESIAN_POINT('Ctrl Pts',(-1.30011459796815,13.4740957862082,21.1220490156415));
#32818=CARTESIAN_POINT('Ctrl Pts',(-7.58916284073994,11.4071970410936,21.3954865156415));
#32819=CARTESIAN_POINT('Ctrl Pts',(-12.2161225976628,6.55956001405331,21.6689240156415));
#32820=CARTESIAN_POINT('Ctrl Pts',(-13.4238578627515,2.20508272349997,21.8512156823082));
#32821=CARTESIAN_POINT('Ctrl Pts',(-13.476480934162,1.65039292397919E-14,
21.9423615156415));
#32822=CARTESIAN_POINT('Ctrl Pts',(-2.98371143764262,0.,4.75150716662327));
#32823=CARTESIAN_POINT('Ctrl Pts',(-3.03633450905313,-0.488281981545911,
4.84265299995661));
#32824=CARTESIAN_POINT('Ctrl Pts',(-2.89719239750444,-1.51773468502555,
5.02494466662328));
#32825=CARTESIAN_POINT('Ctrl Pts',(-1.93074584541099,-2.84112667747553,
5.29838216662328));
#32826=CARTESIAN_POINT('Ctrl Pts',(-0.37967317259002,-3.57924728657917,
5.57181966662327));
#32827=CARTESIAN_POINT('Ctrl Pts',(1.415345489773,-3.48748570044128,5.84525716662328));
#32828=CARTESIAN_POINT('Ctrl Pts',(3.0192337330702,-2.51273432159306,6.11869466662327));
#32829=CARTESIAN_POINT('Ctrl Pts',(4.0084258174915,-0.824853742020043,6.39213216662327));
#32830=CARTESIAN_POINT('Ctrl Pts',(4.0812172121738,1.20981809279467,6.66556966662328));
#32831=CARTESIAN_POINT('Ctrl Pts',(3.14522441136627,3.10704687470915,6.93900716662327));
#32832=CARTESIAN_POINT('Ctrl Pts',(1.35689553916174,4.38009475553567,7.21244466662328));
#32833=CARTESIAN_POINT('Ctrl Pts',(-0.900149835328617,4.66372673795749,
7.48588216662327));
#32834=CARTESIAN_POINT('Ctrl Pts',(-3.09659020305971,3.81575732694958,7.75931966662327));
#32835=CARTESIAN_POINT('Ctrl Pts',(-4.68152436880527,1.96836908930344,8.03275716662328));
#32836=CARTESIAN_POINT('Ctrl Pts',(-5.22017806292132,-0.487017834823588,
8.30619466662326));
#32837=CARTESIAN_POINT('Ctrl Pts',(-4.51085999202353,-2.98159470334547,
8.57963216662328));
#32838=CARTESIAN_POINT('Ctrl Pts',(-2.65018374428007,-4.90088080835761,
8.85306966662327));
#32839=CARTESIAN_POINT('Ctrl Pts',(-0.0269941662667494,-5.73582968895438,
9.12650716662328));
#32840=CARTESIAN_POINT('Ctrl Pts',(2.7575190506044,-5.2162195105121,9.39994466662327));
#32841=CARTESIAN_POINT('Ctrl Pts',(5.02747616549161,-3.39171778792666,9.67338216662326));
#32842=CARTESIAN_POINT('Ctrl Pts',(6.19624214645689,-0.637401365670468,
9.94681966662328));
#32843=CARTESIAN_POINT('Ctrl Pts',(5.91690688753647,2.42164480220557,10.2202571666233));
#32844=CARTESIAN_POINT('Ctrl Pts',(4.18095353060857,5.05195546011693,10.4936946666233));
#32845=CARTESIAN_POINT('Ctrl Pts',(1.33785973807176,6.58750755266943,10.7671321666233));
#32846=CARTESIAN_POINT('Ctrl Pts',(-1.97315110464824,6.59759952609516,11.0405696666233));
#32847=CARTESIAN_POINT('Ctrl Pts',(-4.96646430429082,5.00463982355861,11.3140071666233));
#32848=CARTESIAN_POINT('Ctrl Pts',(-6.89647518179741,2.12023170635493,11.5874446666233));
#32849=CARTESIAN_POINT('Ctrl Pts',(-7.24281117446687,-1.41316170161731,
11.8608821666233));
#32850=CARTESIAN_POINT('Ctrl Pts',(-5.84847418872696,-4.76479789289847,
12.1343196666233));
#32851=CARTESIAN_POINT('Ctrl Pts',(-2.9746778656042,-7.11096848502258,12.4077571666233));
#32852=CARTESIAN_POINT('Ctrl Pts',(0.744764861625225,-7.83712707009927,
12.6811946666233));
#32853=CARTESIAN_POINT('Ctrl Pts',(4.44252845630195,-6.69730190823927,12.9546321666233));
#32854=CARTESIAN_POINT('Ctrl Pts',(7.21999096207501,-3.88977393637157,13.2280696666233));
#32855=CARTESIAN_POINT('Ctrl Pts',(8.36544100612696,-0.0269941685586301,
13.5015071666233));
#32856=CARTESIAN_POINT('Ctrl Pts',(7.53532965583381,3.99710924842502,13.7749446666233));
#32857=CARTESIAN_POINT('Ctrl Pts',(4.85265156187039,7.21391807196961,14.0483821666233));
#32858=CARTESIAN_POINT('Ctrl Pts',(0.895148348404636,8.81319117224774,14.3218196666233));
#32859=CARTESIAN_POINT('Ctrl Pts',(-3.42795348933533,8.34635096696369,14.5952571666233));
#32860=CARTESIAN_POINT('Ctrl Pts',(-7.08467250073323,5.84916129380098,14.8686946666232));
#32861=CARTESIAN_POINT('Ctrl Pts',(-9.16659163129478,1.85087145778383,15.1421321666233));
#32862=CARTESIAN_POINT('Ctrl Pts',(-9.11398066814341,-2.73648697878813,
15.4155696666233));
#32863=CARTESIAN_POINT('Ctrl Pts',(-6.86405582172724,-6.82588030247055,
15.6890071666233));
#32864=CARTESIAN_POINT('Ctrl Pts',(-2.88356758061773,-9.41285632394088,
15.9624446666233));
#32865=CARTESIAN_POINT('Ctrl Pts',(1.92617342162557,-9.82189525284306,16.2358821666233));
#32866=CARTESIAN_POINT('Ctrl Pts',(6.43300565547342,-7.88119122987088,16.5093196666233));
#32867=CARTESIAN_POINT('Ctrl Pts',(9.54041256569715,-3.98098655166418,16.7827571666233));
#32868=CARTESIAN_POINT('Ctrl Pts',(10.4540760933895,1.00251184221285,17.0561946666233));
#32869=CARTESIAN_POINT('Ctrl Pts',(8.88374381972081,5.90346223454177,17.3296321666233));
#32870=CARTESIAN_POINT('Ctrl Pts',(5.12936412418515,9.53910109880408,17.6030696666233));
#32871=CARTESIAN_POINT('Ctrl Pts',(0.0269941862784956,10.9950523404831,
17.8765071666233));
#32872=CARTESIAN_POINT('Ctrl Pts',(-5.23669948053405,9.85443977518913,18.1499446666233));
#32873=CARTESIAN_POINT('Ctrl Pts',(-9.40035990816268,6.31358538354047,18.4233821666233));
#32874=CARTESIAN_POINT('Ctrl Pts',(-11.4301403394459,1.15289523780071,18.6968196666233));
#32875=CARTESIAN_POINT('Ctrl Pts',(-10.7757947631911,-4.43426199086815,
18.9702571666232));
#32876=CARTESIAN_POINT('Ctrl Pts',(-7.51736962351869,-9.11738991195976,
19.2436946666233));
#32877=CARTESIAN_POINT('Ctrl Pts',(-2.3638820445165,-11.7456749690791,19.5171321666233));
#32878=CARTESIAN_POINT('Ctrl Pts',(3.49982058727274,-11.6303632915086,19.7905696666233));
#32879=CARTESIAN_POINT('Ctrl Pts',(8.68530083127351,-8.72346885779468,20.0640071666233));
#32880=CARTESIAN_POINT('Ctrl Pts',(11.9292284062458,-3.64690937811811,20.3374446666233));
#32881=CARTESIAN_POINT('Ctrl Pts',(12.4009974481478,2.43919698625482,20.6108821666233));
#32882=CARTESIAN_POINT('Ctrl Pts',(9.91387204151406,8.10118973214408,20.8843196666233));
#32883=CARTESIAN_POINT('Ctrl Pts',(4.98736770327087,11.9699040160853,21.1577571666233));
#32884=CARTESIAN_POINT('Ctrl Pts',(-1.26040396668559,13.070930321012,21.4311946666233));
#32885=CARTESIAN_POINT('Ctrl Pts',(-7.36410254721529,11.0703762347581,21.7046321666233));
#32886=CARTESIAN_POINT('Ctrl Pts',(-11.8588354668916,6.36856091485502,21.9780696666233));
#32887=CARTESIAN_POINT('Ctrl Pts',(-13.0347180770506,2.14148452707192,22.1603613332899));
#32888=CARTESIAN_POINT('Ctrl Pts',(-13.0873411484611,1.60273704468123E-14,
22.2515071666233));
#32889=CARTESIAN_POINT('Ctrl Pts',(-2.98483377249807,0.,5.2480277325673));
#32890=CARTESIAN_POINT('Ctrl Pts',(-3.03745684390858,-0.488306844967222,
5.33917356590063));
#32891=CARTESIAN_POINT('Ctrl Pts',(-2.89820050196772,-1.51837199860867,
5.5214652325673));
#32892=CARTESIAN_POINT('Ctrl Pts',(-1.93138996818963,-2.84204079236029,
5.7949027325673));
#32893=CARTESIAN_POINT('Ctrl Pts',(-0.379784218761552,-3.58041598369861,
6.0683402325673));
#32894=CARTESIAN_POINT('Ctrl Pts',(1.41578555107907,-3.48853951372869,6.3417777325673));
#32895=CARTESIAN_POINT('Ctrl Pts',(3.02012505022879,-2.51347086100097,6.6152152325673));
#32896=CARTESIAN_POINT('Ctrl Pts',(4.00955586475944,-0.825075846581511,
6.88865273256729));
#32897=CARTESIAN_POINT('Ctrl Pts',(4.08232013773346,1.21015126356688,7.1620902325673));
#32898=CARTESIAN_POINT('Ctrl Pts',(3.14603924239308,3.10786244643203,7.43552773256729));
#32899=CARTESIAN_POINT('Ctrl Pts',(1.35723010161685,4.38119722121209,7.7089652325673));
#32900=CARTESIAN_POINT('Ctrl Pts',(-0.900374678086592,4.66485719413016,
7.9824027325673));
#32901=CARTESIAN_POINT('Ctrl Pts',(-3.09732128911458,3.81664808180835,8.2558402325673));
#32902=CARTESIAN_POINT('Ctrl Pts',(-4.68258907853753,1.96881014756007,8.52927773256729));
#32903=CARTESIAN_POINT('Ctrl Pts',(-5.22132494126317,-0.487130813963699,
8.8027152325673));
#32904=CARTESIAN_POINT('Ctrl Pts',(-4.511818203042,-2.98223494820395,9.0761527325673));
#32905=CARTESIAN_POINT('Ctrl Pts',(-2.65072699530537,-4.90189716574,9.3495902325673));
#32906=CARTESIAN_POINT('Ctrl Pts',(-0.0269941665001183,-5.73698211576155,
9.6230277325673));
#32907=CARTESIAN_POINT('Ctrl Pts',(2.75806230221306,-5.21723586390009,9.89646523256729));
#32908=CARTESIAN_POINT('Ctrl Pts',(5.02843437551854,-3.39235804277017,10.1699027325673));
#32909=CARTESIAN_POINT('Ctrl Pts',(6.19738902669399,-0.63751432384474,10.4433402325673));
#32910=CARTESIAN_POINT('Ctrl Pts',(5.91797159352262,2.4220858180376,10.7167777325673));
#32911=CARTESIAN_POINT('Ctrl Pts',(4.18168462413262,5.05284630006133,10.9902152325673));
#32912=CARTESIAN_POINT('Ctrl Pts',(1.33808456590467,6.58863783857275,11.2636527325673));
#32913=CARTESIAN_POINT('Ctrl Pts',(-1.97348563726341,6.59870233231904,11.5370902325673));
#32914=CARTESIAN_POINT('Ctrl Pts',(-4.96727919498537,5.00545471426267,11.8105277325673));
#32915=CARTESIAN_POINT('Ctrl Pts',(-6.89757798804165,2.12056623896671,12.0839652325673));
#32916=CARTESIAN_POINT('Ctrl Pts',(-7.24394146032877,-1.41338652945127,
12.3574027325673));
#32917=CARTESIAN_POINT('Ctrl Pts',(-5.84936502875454,-4.76552898641652,
12.6308402325673));
#32918=CARTESIAN_POINT('Ctrl Pts',(-2.97511888126971,-7.11203319102266,
12.9042777325673));
#32919=CARTESIAN_POINT('Ctrl Pts',(0.744877819466415,-7.83827395030751,
13.1777152325673));
#32920=CARTESIAN_POINT('Ctrl Pts',(4.44316871181156,-6.6982601183244,13.4511527325673));
#32921=CARTESIAN_POINT('Ctrl Pts',(7.22100731413099,-3.8903171878636,13.7245902325673));
#32922=CARTESIAN_POINT('Ctrl Pts',(8.36659343559775,-0.0269941685586248,
13.9980277325673));
#32923=CARTESIAN_POINT('Ctrl Pts',(7.53634600788979,3.99765249991704,14.2714652325673));
#32924=CARTESIAN_POINT('Ctrl Pts',(4.85329181738001,7.21487628205475,14.5449027325673));
#32925=CARTESIAN_POINT('Ctrl Pts',(0.895261306245823,8.81433805245597,14.8183402325673));
#32926=CARTESIAN_POINT('Ctrl Pts',(-3.42839450500082,8.34741567296378,15.0917777325673));
#32927=CARTESIAN_POINT('Ctrl Pts',(-7.08556334076082,5.84989238731903,15.3652152325673));
#32928=CARTESIAN_POINT('Ctrl Pts',(-9.16772191715667,1.85109628561778,15.6386527325673));
#32929=CARTESIAN_POINT('Ctrl Pts',(-9.11508347438764,-2.73682151139992,
15.9120902325673));
#32930=CARTESIAN_POINT('Ctrl Pts',(-6.8648707124218,-6.8266951931746,16.1855277325673));
#32931=CARTESIAN_POINT('Ctrl Pts',(-2.88390211323289,-9.41395913016475,
16.4589652325673));
#32932=CARTESIAN_POINT('Ctrl Pts',(1.92639824945848,-9.82302553874637,16.7324027325673));
#32933=CARTESIAN_POINT('Ctrl Pts',(6.43373674899746,-7.88208206981527,17.0058402325673));
#32934=CARTESIAN_POINT('Ctrl Pts',(9.54147727168329,-3.98142756749621,17.2792777325673));
#32935=CARTESIAN_POINT('Ctrl Pts',(10.4552229736266,1.00262480038713,17.5527152325673));
#32936=CARTESIAN_POINT('Ctrl Pts',(8.88470202974774,5.90410248938528,17.8261527325673));
#32937=CARTESIAN_POINT('Ctrl Pts',(5.12990737579382,9.54011745219205,18.0995902325673));
#32938=CARTESIAN_POINT('Ctrl Pts',(0.0269941860451295,10.9962047672903,
18.3730277325673));
#32939=CARTESIAN_POINT('Ctrl Pts',(-5.23724273155935,9.8554561325715,18.6464652325673));
#32940=CARTESIAN_POINT('Ctrl Pts',(-9.40131811918114,6.31422562839895,18.9199027325673));
#32941=CARTESIAN_POINT('Ctrl Pts',(-11.4312872177877,1.15300821694082,19.1933402325673));
#32942=CARTESIAN_POINT('Ctrl Pts',(-10.7768594729234,-4.43470304912478,
19.4667777325673));
#32943=CARTESIAN_POINT('Ctrl Pts',(-7.51810070957355,-9.11828066681853,
19.7402152325673));
#32944=CARTESIAN_POINT('Ctrl Pts',(-2.36410688727448,-11.7468054252518,
20.0136527325673));
#32945=CARTESIAN_POINT('Ctrl Pts',(3.50015514972786,-11.631465757185,20.2870902325673));
#32946=CARTESIAN_POINT('Ctrl Pts',(8.6861156623003,-8.72428442951756,20.5605277325673));
#32947=CARTESIAN_POINT('Ctrl Pts',(11.9303313318055,-3.64724254889032,20.8339652325673));
#32948=CARTESIAN_POINT('Ctrl Pts',(12.4021274954157,2.43941909081629,21.1074027325673));
#32949=CARTESIAN_POINT('Ctrl Pts',(9.91476335867265,8.10192627155198,21.3808402325673));
#32950=CARTESIAN_POINT('Ctrl Pts',(4.98780776457694,11.9709578293727,21.6542777325673));
#32951=CARTESIAN_POINT('Ctrl Pts',(-1.26051501285712,13.0720990181314,21.9277152325673));
#32952=CARTESIAN_POINT('Ctrl Pts',(-7.36474666999395,11.0712903496429,22.2011527325673));
#32953=CARTESIAN_POINT('Ctrl Pts',(-11.8598435713549,6.36919822843813,22.4745902325673));
#32954=CARTESIAN_POINT('Ctrl Pts',(-13.035840411906,2.14150939049322,22.656881899234));
#32955=CARTESIAN_POINT('Ctrl Pts',(-13.0884634833165,1.60287449106006E-14,
22.7480277325673));
#32956=CARTESIAN_POINT('Ctrl Pts',(-3.37236445914593,0.,5.55880118622959));
#32957=CARTESIAN_POINT('Ctrl Pts',(-3.42498753055644,-0.551891116017674,
5.64994701956293));
#32958=CARTESIAN_POINT('Ctrl Pts',(-3.25404537003884,-1.70844553497412,
5.83223868622959));
#32959=CARTESIAN_POINT('Ctrl Pts',(-2.15552746120626,-3.17755887888968,
6.10567618622959));
#32960=CARTESIAN_POINT('Ctrl Pts',(-0.419336119804426,-3.98190507031525,
6.37911368622959));
#32961=CARTESIAN_POINT('Ctrl Pts',(1.57018554686087,-3.86130025668376,6.65255118622959));
#32962=CARTESIAN_POINT('Ctrl Pts',(3.33200139390039,-2.76941567544733,6.92598868622959));
#32963=CARTESIAN_POINT('Ctrl Pts',(4.40526304098788,-0.903790108850918,
7.19942618622959));
#32964=CARTESIAN_POINT('Ctrl Pts',(4.46840573366961,1.32727084336026,7.47286368622959));
#32965=CARTESIAN_POINT('Ctrl Pts',(3.43132786358059,3.39315003911043,7.74630118622959));
#32966=CARTESIAN_POINT('Ctrl Pts',(1.47434790676726,4.76728361353632,8.01973868622959));
#32967=CARTESIAN_POINT('Ctrl Pts',(-0.979085532660522,5.06056340808148,
8.29317618622959));
#32968=CARTESIAN_POINT('Ctrl Pts',(-3.353272847575,4.12852603461372,8.56661368622959));
#32969=CARTESIAN_POINT('Ctrl Pts',(-5.05533636777526,2.1232070824127,8.84005118622959));
#32970=CARTESIAN_POINT('Ctrl Pts',(-5.62284095416809,-0.526676662681731,
9.11348868622958));
#32971=CARTESIAN_POINT('Ctrl Pts',(-4.84728190823904,-3.20638464492345,
9.3869261862296));
#32972=CARTESIAN_POINT('Ctrl Pts',(-2.84091614500297,-5.25771602884916,
9.66036368622959));
#32973=CARTESIAN_POINT('Ctrl Pts',(-0.026994165764487,-6.14044089033148,
9.93380118622959));
#32974=CARTESIAN_POINT('Ctrl Pts',(2.94825145007176,-5.57305473193853,10.2072386862296));
#32975=CARTESIAN_POINT('Ctrl Pts',(5.36389808384115,-3.61650772716763,10.4806761862296));
#32976=CARTESIAN_POINT('Ctrl Pts',(6.59890503362463,-0.67706019843569,10.7541136862296));
#32977=CARTESIAN_POINT('Ctrl Pts',(6.29071889456904,2.57648280524436,11.0275511862296));
#32978=CARTESIAN_POINT('Ctrl Pts',(4.43763615904838,5.36472414786668,11.3009886862296));
#32979=CARTESIAN_POINT('Ctrl Pts',(1.41679546752599,6.98434426264517,11.5744261862296));
#32980=CARTESIAN_POINT('Ctrl Pts',(-2.09060353647649,6.98478830439027,11.8478636862296));
#32981=CARTESIAN_POINT('Ctrl Pts',(-5.25256762808581,5.29074314735314,12.1213011862296));
#32982=CARTESIAN_POINT('Ctrl Pts',(-7.28366396008863,2.23768413818047,12.3947386862296));
#32983=CARTESIAN_POINT('Ctrl Pts',(-7.63964788445187,-1.49209743106429,
12.6681761862296));
#32984=CARTESIAN_POINT('Ctrl Pts',(-6.16124287645745,-5.02148052135369,
12.9416136862296));
#32985=CARTESIAN_POINT('Ctrl Pts',(-3.12951586868186,-7.48478049202387,
13.2150511862296));
#32986=CARTESIAN_POINT('Ctrl Pts',(0.784423694468346,-8.23978995732977,
13.4884886862296));
#32987=CARTESIAN_POINT('Ctrl Pts',(4.66731839538705,-7.03372382646324,13.7619261862296));
#32988=CARTESIAN_POINT('Ctrl Pts',(7.57682618381319,-4.08050633609009,14.0353636862296));
#32989=CARTESIAN_POINT('Ctrl Pts',(8.77005220688066,-0.0269941685586276,
14.3088011862296));
#32990=CARTESIAN_POINT('Ctrl Pts',(7.89216487757199,4.18784164814354,14.5822386862296));
#32991=CARTESIAN_POINT('Ctrl Pts',(5.07744150095549,7.55033999019357,14.8556761862296));
#32992=CARTESIAN_POINT('Ctrl Pts',(0.934807181247757,9.21585405947824,15.1291136862296));
#32993=CARTESIAN_POINT('Ctrl Pts',(-3.58279149241298,8.72016297396498,15.4025511862296));
#32994=CARTESIAN_POINT('Ctrl Pts',(-7.39744118846373,6.1058439222562,15.6759886862296));
#32995=CARTESIAN_POINT('Ctrl Pts',(-9.56342834127977,1.9298071872308,15.9494261862296));
#32996=CARTESIAN_POINT('Ctrl Pts',(-9.50116944643463,-2.85393941061368,
16.2228636862296));
#32997=CARTESIAN_POINT('Ctrl Pts',(-7.15015914552224,-7.11198362626506,
16.4963011862296));
#32998=CARTESIAN_POINT('Ctrl Pts',(-3.00102001244598,-9.800045102236,16.7697386862296));
#32999=CARTESIAN_POINT('Ctrl Pts',(2.00510915107979,-10.2187319628188,17.0431761862296));
#33000=CARTESIAN_POINT('Ctrl Pts',(6.68968828391324,-8.19395991762063,17.3166136862296));
#33001=CARTESIAN_POINT('Ctrl Pts',(9.91422457272969,-4.13582455470297,17.5900511862296));
#33002=CARTESIAN_POINT('Ctrl Pts',(10.8567389805573,1.04217067497807,17.8634886862296));
#33003=CARTESIAN_POINT('Ctrl Pts',(9.22016573807034,6.12825217378274,18.1369261862296));
#33004=CARTESIAN_POINT('Ctrl Pts',(5.32009652365252,9.89593632023051,18.4103636862296));
#33005=CARTESIAN_POINT('Ctrl Pts',(0.0269941867807571,11.3996635418602,
18.6838011862296));
#33006=CARTESIAN_POINT('Ctrl Pts',(-5.42743188125695,10.2112749956807,18.9572386862296));
#33007=CARTESIAN_POINT('Ctrl Pts',(-9.73678182437819,6.53837532511846,19.2306761862296));
#33008=CARTESIAN_POINT('Ctrl Pts',(-11.8328032306926,1.19255406565886,19.5041136862296));
#33009=CARTESIAN_POINT('Ctrl Pts',(-11.1496067621611,-4.58909998397742,
19.7775511862296));
#33010=CARTESIAN_POINT('Ctrl Pts',(-7.77405226803399,-9.43015861962389,
20.0509886862296));
#33011=CARTESIAN_POINT('Ctrl Pts',(-2.44281774184841,-12.1425116392031,
20.3244261862296));
#33012=CARTESIAN_POINT('Ctrl Pts',(3.61727295487827,-12.0175521495093,20.5978636862296));
#33013=CARTESIAN_POINT('Ctrl Pts',(8.97140428348781,-9.00957202219596,20.8713011862296));
#33014=CARTESIAN_POINT('Ctrl Pts',(12.3164169277416,-3.7643621286837,21.1447386862296));
#33015=CARTESIAN_POINT('Ctrl Pts',(12.7978346716442,2.5181333530857,21.4181761862296));
#33016=CARTESIAN_POINT('Ctrl Pts',(10.2266397023443,8.35787108599834,21.6916136862296));
#33017=CARTESIAN_POINT('Ctrl Pts',(5.14220776035875,12.3437185723278,21.9650511862296));
#33018=CARTESIAN_POINT('Ctrl Pts',(-1.3000669139,13.473588104748,22.2384886862296));
#33019=CARTESIAN_POINT('Ctrl Pts',(-7.58888416301056,11.4068084361723,22.5119261862296));
#33020=CARTESIAN_POINT('Ctrl Pts',(-12.215688439426,6.55927176480358,22.7853636862296));
#33021=CARTESIAN_POINT('Ctrl Pts',(-13.4233710985539,2.20509366154368,22.9676553528962));
#33022=CARTESIAN_POINT('Ctrl Pts',(-13.4759941699644,1.65033331255753E-14,
23.0588011862296));
#33023=CARTESIAN_POINT('Ctrl Pts',(-3.85691369956507,0.,5.4468630354969));
#33024=CARTESIAN_POINT('Ctrl Pts',(-3.90953677097559,-0.630966749404783,
5.53800886883023));
#33025=CARTESIAN_POINT('Ctrl Pts',(-3.69891600544325,-1.9463368927696,5.7203005354969));
#33026=CARTESIAN_POINT('Ctrl Pts',(-2.43576449828385,-3.59691976012222,
5.99373803549689));
#33027=CARTESIAN_POINT('Ctrl Pts',(-0.468780479590593,-4.48392312081373,
6.2671755354969));
#33028=CARTESIAN_POINT('Ctrl Pts',(1.76322064804953,-4.32731286998429,6.5406130354969));
#33029=CARTESIAN_POINT('Ctrl Pts',(3.72192424077144,-3.08942381824181,6.81405053549689));
#33030=CARTESIAN_POINT('Ctrl Pts',(4.899992955087,-1.00219482411329,7.08748803549689));
#33031=CARTESIAN_POINT('Ctrl Pts',(4.95110729194826,1.47369524249325,7.36092553549689));
#33032=CARTESIAN_POINT('Ctrl Pts',(3.78800811550593,3.7498309986416,7.63436303549691));
#33033=CARTESIAN_POINT('Ctrl Pts',(1.62077383149999,5.24998492856633,7.90780053549689));
#33034=CARTESIAN_POINT('Ctrl Pts',(-1.07749335397341,5.55529322263726,8.18123803549691));
#33035=CARTESIAN_POINT('Ctrl Pts',(-3.67327475134075,4.51844937359048,8.4546755354969));
#33036=CARTESIAN_POINT('Ctrl Pts',(-5.52136147425963,2.31624105270174,8.7281130354969));
#33037=CARTESIAN_POINT('Ctrl Pts',(-6.12483397232732,-0.576118683725451,
9.0015505354969));
#33038=CARTESIAN_POINT('Ctrl Pts',(-5.26669342645748,-3.48662645044473,
9.2749880354969));
#33039=CARTESIAN_POINT('Ctrl Pts',(-3.07869900462109,-5.70257647480552,
9.5484255354969));
#33040=CARTESIAN_POINT('Ctrl Pts',(-0.0269941654760016,-6.64486283266747,
9.8218630354969));
#33041=CARTESIAN_POINT('Ctrl Pts',(3.18603430896873,-6.01791517331201,10.0953005354969));
#33042=CARTESIAN_POINT('Ctrl Pts',(5.7833096032853,-3.89674954414503,10.3687380354969));
#33043=CARTESIAN_POINT('Ctrl Pts',(7.10089804944101,-0.726502195424679,
10.6421755354969));
#33044=CARTESIAN_POINT('Ctrl Pts',(6.7567440056843,2.76951672685838,10.9156130354969));
#33045=CARTESIAN_POINT('Ctrl Pts',(4.75763805358084,5.75464758446472,11.1890505354969));
#33046=CARTESIAN_POINT('Ctrl Pts',(1.51520330728903,7.47907388184584,11.4624880354969));
#33047=CARTESIAN_POINT('Ctrl Pts',(-2.23702949809695,7.46749001014054,11.7359255354969));
#33048=CARTESIAN_POINT('Ctrl Pts',(-5.6092478062507,5.64742332553111,12.0093630354969));
#33049=CARTESIAN_POINT('Ctrl Pts',(-7.76636566586335,2.38411009979269,12.2828005354969));
#33050=CARTESIAN_POINT('Ctrl Pts',(-8.13437750360446,-1.59050527081984,
12.5562380354969));
#33051=CARTESIAN_POINT('Ctrl Pts',(-6.55116631315121,-5.34148241589666,
12.8296755354969));
#33052=CARTESIAN_POINT('Ctrl Pts',(-3.32254979010469,-7.95080560312036,
13.1031130354969));
#33053=CARTESIAN_POINT('Ctrl Pts',(0.833865691075113,-8.74178297318257,
13.3765505354969));
#33054=CARTESIAN_POINT('Ctrl Pts',(4.94756021312872,-7.45313534583507,13.6499880354969));
#33055=CARTESIAN_POINT('Ctrl Pts',(8.02168662365838,-4.3182891951314,13.9234255354969));
#33056=CARTESIAN_POINT('Ctrl Pts',(9.27447415227271,-0.0269941685586289,
14.1968630354969));
#33057=CARTESIAN_POINT('Ctrl Pts',(8.33702531741718,4.42562450718485,14.4703005354969));
#33058=CARTESIAN_POINT('Ctrl Pts',(5.35768331869717,7.96975150956542,14.7437380354969));
#33059=CARTESIAN_POINT('Ctrl Pts',(0.984249177854521,9.71784707533104,15.0171755354969));
#33060=CARTESIAN_POINT('Ctrl Pts',(-3.77582541383581,9.18618808506149,15.2906130354969));
#33061=CARTESIAN_POINT('Ctrl Pts',(-7.78736462515749,6.42584581679915,15.5640505354969));
#33062=CARTESIAN_POINT('Ctrl Pts',(-10.0581579604324,2.02821502698636,15.8374880354969));
#33063=CARTESIAN_POINT('Ctrl Pts',(-9.98387115220935,-3.0003653722259,16.1109255354969));
#33064=CARTESIAN_POINT('Ctrl Pts',(-7.50683932368714,-7.46866380444304,
16.3843630354969));
#33065=CARTESIAN_POINT('Ctrl Pts',(-3.14744597406643,-10.2827468079863,
16.6578005354969));
#33066=CARTESIAN_POINT('Ctrl Pts',(2.10351699084284,-10.7134615820195,16.9312380354969));
#33067=CARTESIAN_POINT('Ctrl Pts',(7.00969017844569,-8.58388335421866,17.2046755354969));
#33068=CARTESIAN_POINT('Ctrl Pts',(10.380249683845,-4.328858476317,17.4781130354969));
#33069=CARTESIAN_POINT('Ctrl Pts',(11.3587319963737,1.09161267196707,17.7515505354969));
#33070=CARTESIAN_POINT('Ctrl Pts',(9.63957725751449,6.40849399076014,18.0249880354969));
#33071=CARTESIAN_POINT('Ctrl Pts',(5.55787938254949,10.340796761604,18.2984255354969));
#33072=CARTESIAN_POINT('Ctrl Pts',(0.0269941870692434,11.9040854841962,
18.5718630354969));
#33073=CARTESIAN_POINT('Ctrl Pts',(-5.66521474087506,10.656135441637,18.8453005354969));
#33074=CARTESIAN_POINT('Ctrl Pts',(-10.1561933425966,6.81861713063972,19.1187380354969));
#33075=CARTESIAN_POINT('Ctrl Pts',(-12.3347962488519,1.24199608670258,19.3921755354969));
#33076=CARTESIAN_POINT('Ctrl Pts',(-11.6156318686455,-4.78213395426646,
19.6656130354969));
#33077=CARTESIAN_POINT('Ctrl Pts',(-8.09405417179972,-9.82008195860066,
19.9390505354969));
#33078=CARTESIAN_POINT('Ctrl Pts',(-2.5412255631613,-12.6372414537589,20.2124880354969));
#33079=CARTESIAN_POINT('Ctrl Pts',(3.76369887961099,-12.5002534645393,20.4859255354969));
#33080=CARTESIAN_POINT('Ctrl Pts',(9.32808453541316,-9.36625298172713,20.7593630354969));
#33081=CARTESIAN_POINT('Ctrl Pts',(12.7991184860202,-3.91078652781669,21.0328005354969));
#33082=CARTESIAN_POINT('Ctrl Pts',(13.2925645857433,2.61653806834808,21.3062380354969));
#33083=CARTESIAN_POINT('Ctrl Pts',(10.6165625492153,8.67787922879281,21.5796755354969));
#33084=CARTESIAN_POINT('Ctrl Pts',(5.33524286154741,12.8097311856283,21.8531130354969));
#33085=CARTESIAN_POINT('Ctrl Pts',(-1.34951127368616,13.9756061552465,22.1265505354969));
#33086=CARTESIAN_POINT('Ctrl Pts',(-7.86912120008815,11.8261693174048,22.3999880354969));
#33087=CARTESIAN_POINT('Ctrl Pts',(-12.6605590748304,6.79716312259906,22.6734255354969));
#33088=CARTESIAN_POINT('Ctrl Pts',(-13.907920338973,2.28416929493079,22.8557172021636));
#33089=CARTESIAN_POINT('Ctrl Pts',(-13.9605434103835,1.70967348018838E-14,
22.9468630354969));
#33090=CARTESIAN_POINT('Ctrl Pts',(-4.,0.,5.14959965017094));
#33091=CARTESIAN_POINT('Ctrl Pts',(-4.05262307141051,-0.654750131429363,
5.24074548350428));
#33092=CARTESIAN_POINT('Ctrl Pts',(-3.8303463039323,-2.01634987255655,5.42303715017094));
#33093=CARTESIAN_POINT('Ctrl Pts',(-2.51853145823641,-3.72091245378127,
5.69647465017095));
#33094=CARTESIAN_POINT('Ctrl Pts',(-0.483390794043284,-4.63215179981628,
5.96991215017094));
#33095=CARTESIAN_POINT('Ctrl Pts',(1.82024275704298,-4.46499525782153,6.24334965017094));
#33096=CARTESIAN_POINT('Ctrl Pts',(3.83709993106723,-3.18393428471325,6.51678715017094));
#33097=CARTESIAN_POINT('Ctrl Pts',(5.04612894468598,-1.03126943103203,6.79022465017094));
#33098=CARTESIAN_POINT('Ctrl Pts',(5.09368931613234,1.51695038887847,7.06366215017095));
#33099=CARTESIAN_POINT('Ctrl Pts',(3.89336594368056,3.85518701637207,7.33709965017094));
#33100=CARTESIAN_POINT('Ctrl Pts',(1.66402563541432,5.39256813596453,7.61053715017095));
#33101=CARTESIAN_POINT('Ctrl Pts',(-1.10656141591542,5.70142806492059,7.88397465017094));
#33102=CARTESIAN_POINT('Ctrl Pts',(-3.76779823668917,4.63362674874576,8.15741215017094));
#33103=CARTESIAN_POINT('Ctrl Pts',(-5.65901785694323,2.3732600965194,8.43084965017094));
#33104=CARTESIAN_POINT('Ctrl Pts',(-6.27311471850686,-0.590723011110406,
8.70428715017094));
#33105=CARTESIAN_POINT('Ctrl Pts',(-5.3905809053663,-3.5694054447107,8.97772465017095));
#33106=CARTESIAN_POINT('Ctrl Pts',(-3.14893627486886,-5.8339811496207,9.25116215017094));
#33107=CARTESIAN_POINT('Ctrl Pts',(-0.0269941647513346,-6.79386104650306,
9.52459965017095));
#33108=CARTESIAN_POINT('Ctrl Pts',(3.256271577405,-6.14931985765915,9.79803715017094));
#33109=CARTESIAN_POINT('Ctrl Pts',(5.90719708527311,-3.97952851458338,10.0714746501709));
#33110=CARTESIAN_POINT('Ctrl Pts',(7.24917878973531,-0.741106572841118,
10.3449121501709));
#33111=CARTESIAN_POINT('Ctrl Pts',(6.89440040000061,2.82653587191529,10.6183496501709));
#33112=CARTESIAN_POINT('Ctrl Pts',(4.85216151573545,5.86982475657732,10.8917871501709));
#33113=CARTESIAN_POINT('Ctrl Pts',(1.54427141557733,7.62520913044859,11.1652246501709));
#33114=CARTESIAN_POINT('Ctrl Pts',(-2.28028139467223,7.61007240487899,11.4386621501709));
#33115=CARTESIAN_POINT('Ctrl Pts',(-5.71460544914113,5.75278096839949,11.7120996501709));
#33116=CARTESIAN_POINT('Ctrl Pts',(-7.9089480605535,2.42736199637475,11.9855371501709));
#33117=CARTESIAN_POINT('Ctrl Pts',(-8.28051275230592,-1.61957337910302,
12.258974650171));
#33118=CARTESIAN_POINT('Ctrl Pts',(-6.66634348506537,-5.43600587807083,
12.5324121501709));
#33119=CARTESIAN_POINT('Ctrl Pts',(-3.37956893555893,-8.0884619973929,12.8058496501709));
#33120=CARTESIAN_POINT('Ctrl Pts',(0.848470069286372,-8.89006371356673,
13.0792871501709));
#33121=CARTESIAN_POINT('Ctrl Pts',(5.03033918197755,-7.57702282764202,13.3527246501709));
#33122=CARTESIAN_POINT('Ctrl Pts',(8.15309131118414,-4.38852646392991,13.6261621501709));
#33123=CARTESIAN_POINT('Ctrl Pts',(9.42347235975202,-0.0269941685586307,
13.8995996501709));
#33124=CARTESIAN_POINT('Ctrl Pts',(8.46843000494294,4.49586177598336,14.1730371501709));
#33125=CARTESIAN_POINT('Ctrl Pts',(5.44046228754599,8.09363899137236,14.446474650171));
#33126=CARTESIAN_POINT('Ctrl Pts',(0.998853556065788,9.86612781571521,14.7199121501709));
#33127=CARTESIAN_POINT('Ctrl Pts',(-3.83284455929006,9.32384447933402,14.993349650171));
#33128=CARTESIAN_POINT('Ctrl Pts',(-7.90254179707164,6.52036927897334,15.2667871501709));
#33129=CARTESIAN_POINT('Ctrl Pts',(-10.2042932091338,2.05728313526953,15.540224650171));
#33130=CARTESIAN_POINT('Ctrl Pts',(-10.1264535468995,-3.04361726880795,
15.8136621501709));
#33131=CARTESIAN_POINT('Ctrl Pts',(-7.61219696657756,-7.57402144731142,
16.087099650171));
#33132=CARTESIAN_POINT('Ctrl Pts',(-3.19069787064171,-10.4253292027247,
16.3605371501709));
#33133=CARTESIAN_POINT('Ctrl Pts',(2.13258509913113,-10.8595968306222,16.6339746501709));
#33134=CARTESIAN_POINT('Ctrl Pts',(7.10421364060031,-8.69906052633126,16.9074121501709));
#33135=CARTESIAN_POINT('Ctrl Pts',(10.5179060781613,-4.3858776213739,17.1808496501709));
#33136=CARTESIAN_POINT('Ctrl Pts',(11.5070127366679,1.1062170493835,17.4542871501709));
#33137=CARTESIAN_POINT('Ctrl Pts',(9.76346473950231,6.4912729611985,17.7277246501709));
#33138=CARTESIAN_POINT('Ctrl Pts',(5.62811665098576,10.4722014459511,18.0011621501709));
#33139=CARTESIAN_POINT('Ctrl Pts',(0.0269941877939141,12.0530836980318,
18.2745996501709));
#33140=CARTESIAN_POINT('Ctrl Pts',(-5.73545201112284,10.7875401164522,18.5480371501709));
#33141=CARTESIAN_POINT('Ctrl Pts',(-10.2800808215054,6.90139612490571,18.8214746501709));
#33142=CARTESIAN_POINT('Ctrl Pts',(-12.4830769950314,1.25660041408754,19.0949121501709));
#33143=CARTESIAN_POINT('Ctrl Pts',(-11.7532882513291,-4.83915299808411,
19.368349650171));
#33144=CARTESIAN_POINT('Ctrl Pts',(-8.18857765714814,-9.93525933375593,
19.6417871501709));
#33145=CARTESIAN_POINT('Ctrl Pts',(-2.57029362510331,-12.7833762960422,
19.915224650171));
#33146=CARTESIAN_POINT('Ctrl Pts',(3.80695068352532,-12.6428366719375,20.1886621501709));
#33147=CARTESIAN_POINT('Ctrl Pts',(9.43344236358779,-9.4716089994576,20.462099650171));
#33148=CARTESIAN_POINT('Ctrl Pts',(12.9417005102043,-3.95404167420191,20.7355371501709));
#33149=CARTESIAN_POINT('Ctrl Pts',(13.4387005753423,2.6456126752668,21.008974650171));
#33150=CARTESIAN_POINT('Ctrl Pts',(10.7317382395111,8.77238969526427,21.2824121501709));
#33151=CARTESIAN_POINT('Ctrl Pts',(5.39226497054085,12.9474135734656,21.555849650171));
#33152=CARTESIAN_POINT('Ctrl Pts',(-1.36412158813886,14.1238348342491,21.8292871501709));
#33153=CARTESIAN_POINT('Ctrl Pts',(-7.9518881600407,11.9501620110638,22.102724650171));
#33154=CARTESIAN_POINT('Ctrl Pts',(-12.7919893733195,6.86717610238603,22.3761621501709));
#33155=CARTESIAN_POINT('Ctrl Pts',(-14.0510066394079,2.30795267695537,22.5584538168376));
#33156=CARTESIAN_POINT('Ctrl Pts',(-14.1036297108185,1.72719649817133E-14,
22.6495996501709));
#33157=CARTESIAN_POINT('Ctrl Pts',(-4.,0.,5.));
#33158=CARTESIAN_POINT('Ctrl Pts',(-4.05262307141051,-0.654498469497874,
5.09114583333333));
#33159=CARTESIAN_POINT('Ctrl Pts',(-3.83031081101585,-2.0164870728516,5.2734375));
#33160=CARTESIAN_POINT('Ctrl Pts',(-2.51852354898032,-3.7208214715467,5.546875));
#33161=CARTESIAN_POINT('Ctrl Pts',(-0.483385262891241,-4.63216118014149,
5.82031249999999));
#33162=CARTESIAN_POINT('Ctrl Pts',(1.8202315402997,-4.46495458019068,6.09375000000001));
#33163=CARTESIAN_POINT('Ctrl Pts',(3.83708110788313,-3.18392684763,6.36718749999999));
#33164=CARTESIAN_POINT('Ctrl Pts',(5.04610371647275,-1.03126017046504,6.640625));
#33165=CARTESIAN_POINT('Ctrl Pts',(5.09366526266359,1.51694087528755,6.9140625));
#33166=CARTESIAN_POINT('Ctrl Pts',(3.89334793428042,3.85517018194508,7.1875));
#33167=CARTESIAN_POINT('Ctrl Pts',(1.66401832874098,5.39254335225655,7.4609375));
#33168=CARTESIAN_POINT('Ctrl Pts',(-1.10655649717025,5.70140348716183,7.73437499999999));
#33169=CARTESIAN_POINT('Ctrl Pts',(-3.76778215269101,4.63360702978987,8.0078125));
#33170=CARTESIAN_POINT('Ctrl Pts',(-5.65899445677288,2.37325046891981,8.28125));
#33171=CARTESIAN_POINT('Ctrl Pts',(-6.27308950292314,-0.59072056165688,
8.5546875));
#33172=CARTESIAN_POINT('Ctrl Pts',(-5.39055984190282,-3.56939135267172,
8.828125));
#33173=CARTESIAN_POINT('Ctrl Pts',(-3.14892433147632,-5.83395881494245,
9.10156249999999));
#33174=CARTESIAN_POINT('Ctrl Pts',(-0.0269941651234124,-6.79383570767807,
9.375));
#33175=CARTESIAN_POINT('Ctrl Pts',(3.25625963494257,-6.14929751664737,9.64843749999999));
#33176=CARTESIAN_POINT('Ctrl Pts',(5.90717602022873,-3.9795144383767,9.921875));
#33177=CARTESIAN_POINT('Ctrl Pts',(7.24915357717334,-0.741104090144106,
10.1953125));
#33178=CARTESIAN_POINT('Ctrl Pts',(6.89437699385751,2.82652617704715,10.46875));
#33179=CARTESIAN_POINT('Ctrl Pts',(4.85214544364602,5.8698051725334,10.7421875));
#33180=CARTESIAN_POINT('Ctrl Pts',(1.54426647303593,7.62518428271038,11.015625));
#33181=CARTESIAN_POINT('Ctrl Pts',(-2.28027404042269,7.61004816114384,11.2890625));
#33182=CARTESIAN_POINT('Ctrl Pts',(-5.71458753487403,5.75276305414747,11.5625));
#33183=CARTESIAN_POINT('Ctrl Pts',(-7.90892381685067,2.42735464211985,11.8359375));
#33184=CARTESIAN_POINT('Ctrl Pts',(-8.280487904502,-1.61956843656331,12.109375));
#33185=CARTESIAN_POINT('Ctrl Pts',(-6.66632390115336,-5.43598980597183,
12.3828125));
#33186=CARTESIAN_POINT('Ctrl Pts',(-3.37955924042675,-8.08843859127204,
12.65625));
#33187=CARTESIAN_POINT('Ctrl Pts',(0.848467586061227,-8.89003850095873,
12.9296875));
#33188=CARTESIAN_POINT('Ctrl Pts',(5.03032510682704,-7.57700176269046,13.203125));
#33189=CARTESIAN_POINT('Ctrl Pts',(8.15306896806033,-4.38851452128152,13.4765625));
#33190=CARTESIAN_POINT('Ctrl Pts',(9.42344702515047,-0.0269941685586242,
13.75));
#33191=CARTESIAN_POINT('Ctrl Pts',(8.46840766181913,4.49584983333495,14.0234375));
#33192=CARTESIAN_POINT('Ctrl Pts',(5.44044821239548,8.09361792642082,14.296875));
#33193=CARTESIAN_POINT('Ctrl Pts',(0.998851072840637,9.86610260310719,14.5703125));
#33194=CARTESIAN_POINT('Ctrl Pts',(-3.83283486415787,9.32382107321317,14.84375));
#33195=CARTESIAN_POINT('Ctrl Pts',(-7.90252221315964,6.52035320687432,15.1171875));
#33196=CARTESIAN_POINT('Ctrl Pts',(-10.2042683613299,2.05727819272983,15.390625));
#33197=CARTESIAN_POINT('Ctrl Pts',(-10.1264293031967,-3.04360991455306,
15.6640625));
#33198=CARTESIAN_POINT('Ctrl Pts',(-7.61217905231046,-7.57400353305939,
15.9375));
#33199=CARTESIAN_POINT('Ctrl Pts',(-3.19069051639217,-10.4253049589896,
16.2109375));
#33200=CARTESIAN_POINT('Ctrl Pts',(2.13258015658974,-10.859571982884,16.484375));
#33201=CARTESIAN_POINT('Ctrl Pts',(7.10419756851087,-8.69904094228735,16.7578125));
#33202=CARTESIAN_POINT('Ctrl Pts',(10.5178826720182,-4.38586792650576,17.03125));
#33203=CARTESIAN_POINT('Ctrl Pts',(11.506987524106,1.10621456668648,17.3046875));
#33204=CARTESIAN_POINT('Ctrl Pts',(9.76344367445795,6.49125888499182,17.578125));
#33205=CARTESIAN_POINT('Ctrl Pts',(5.62810470852332,10.4721791049393,17.8515625));
#33206=CARTESIAN_POINT('Ctrl Pts',(0.0269941874218459,12.0530583592068,
18.125));
#33207=CARTESIAN_POINT('Ctrl Pts',(-5.73544006773032,10.7875177817739,18.3984375));
#33208=CARTESIAN_POINT('Ctrl Pts',(-10.2800597580419,6.90138203286673,18.671875));
#33209=CARTESIAN_POINT('Ctrl Pts',(-12.4830517794477,1.25659796463401,18.9453125));
#33210=CARTESIAN_POINT('Ctrl Pts',(-11.7532648511587,-4.83914337048452,
19.21875));
#33211=CARTESIAN_POINT('Ctrl Pts',(-8.18856157315,-9.93523961480004,19.4921875));
#33212=CARTESIAN_POINT('Ctrl Pts',(-2.57028870635813,-12.7833517182835,
19.765625));
#33213=CARTESIAN_POINT('Ctrl Pts',(3.80694337685198,-12.6428118882295,20.0390625));
#33214=CARTESIAN_POINT('Ctrl Pts',(9.43342435418766,-9.47159216503061,20.3125));
#33215=CARTESIAN_POINT('Ctrl Pts',(12.9416764567355,-3.95403216061098,20.5859375));
#33216=CARTESIAN_POINT('Ctrl Pts',(13.4386753471291,2.64560341469982,20.859375));
#33217=CARTESIAN_POINT('Ctrl Pts',(10.731719416327,8.77238225818101,21.1328125));
#33218=CARTESIAN_POINT('Ctrl Pts',(5.39225375379758,12.9473728958347,21.40625));
#33219=CARTESIAN_POINT('Ctrl Pts',(-1.36411605698682,14.1238442145743,21.6796875));
#33220=CARTESIAN_POINT('Ctrl Pts',(-7.95188025078462,11.9500710288293,21.953125));
#33221=CARTESIAN_POINT('Ctrl Pts',(-12.791953880403,6.86731330268108,22.2265625));
#33222=CARTESIAN_POINT('Ctrl Pts',(-14.0510066394079,2.30770101502388,22.4088541666667));
#33223=CARTESIAN_POINT('Ctrl Pts',(-14.1036297108185,1.72719649817133E-14,
22.5));
#33224=CARTESIAN_POINT('',(-4.,0.,5.));
#33225=CARTESIAN_POINT('Ctrl Pts',(-4.,0.,5.));
#33226=CARTESIAN_POINT('Ctrl Pts',(-4.,0.,4.99313090468968));
#33227=CARTESIAN_POINT('Ctrl Pts',(-3.99984912800787,-7.31607958282715E-11,
4.98626238012908));
#33228=CARTESIAN_POINT('Ctrl Pts',(-3.99665140600643,-7.31607958282715E-11,
4.91292688069719));
#33229=CARTESIAN_POINT('Ctrl Pts',(-3.97984082732515,-7.31754050494978E-11,
4.84714403296737));
#33230=CARTESIAN_POINT('Ctrl Pts',(-3.92504698362485,-7.31754050494978E-11,
4.73052812084229));
#33231=CARTESIAN_POINT('Ctrl Pts',(-3.88837099959727,-7.3182295505018E-11,
4.6787736262658));
#33232=CARTESIAN_POINT('Ctrl Pts',(-3.79060884070887,-7.3182295505018E-11,
4.58558772856037));
#33233=CARTESIAN_POINT('Ctrl Pts',(-3.73360882255537,-7.3222926866944E-11,
4.5543170883066));
#33234=CARTESIAN_POINT('Ctrl Pts',(-3.62062886145855,-7.3222926866944E-11,
4.51106951053573));
#33235=CARTESIAN_POINT('Ctrl Pts',(-3.55498900661372,-7.33122171618315E-11,
4.49929281521309));
#33236=CARTESIAN_POINT('Ctrl Pts',(-3.42514177672713,-7.33122171618315E-11,
4.50114804373618));
#33237=CARTESIAN_POINT('Ctrl Pts',(-3.36273596280029,-7.34200079994916E-11,
4.51448293356282));
#33238=CARTESIAN_POINT('Ctrl Pts',(-3.24209738586254,-7.34200079994916E-11,
4.56698211807808));
#33239=CARTESIAN_POINT('Ctrl Pts',(-3.18605812158766,-7.35736907335013E-11,
4.60594883894128));
#33240=CARTESIAN_POINT('Ctrl Pts',(-3.10316353487479,-7.35736907335013E-11,
4.69113814536176));
#33241=CARTESIAN_POINT('Ctrl Pts',(-3.06529482757558,-7.36685445914362E-11,
4.7410844949528));
#33242=CARTESIAN_POINT('Ctrl Pts',(-3.01284056824797,-7.36685445914362E-11,
4.86734749872617));
#33243=CARTESIAN_POINT('Ctrl Pts',(-3.00033399986338,-3.99897980483117E-9,
4.93376452822198));
#33244=CARTESIAN_POINT('Ctrl Pts',(-3.00057394652585,-3.99897980483117E-9,
5.06669212380191));
#33245=CARTESIAN_POINT('Ctrl Pts',(-3.01349577924023,-4.99214209269255E-11,
5.13354317521189));
#33246=CARTESIAN_POINT('Ctrl Pts',(-3.06714330922775,-4.99214209269255E-11,
5.26131316399762));
#33247=CARTESIAN_POINT('Ctrl Pts',(-3.10587060337886,-4.98538136835682E-11,
5.31167639465468));
#33248=CARTESIAN_POINT('Ctrl Pts',(-3.18918143195268,-4.98538136835682E-11,
5.39664026609539));
#33249=CARTESIAN_POINT('Ctrl Pts',(-3.24557401970868,-4.97487385594604E-11,
5.43554633184094));
#33250=CARTESIAN_POINT('Ctrl Pts',(-3.36161420616976,-4.97487385594604E-11,
5.48509146894737));
#33251=CARTESIAN_POINT('Ctrl Pts',(-3.42258429650568,-4.96782254655346E-11,
5.49971498392992));
#33252=CARTESIAN_POINT('Ctrl Pts',(-3.55707996410541,-4.96782254655346E-11,
5.50070596657406));
#33253=CARTESIAN_POINT('Ctrl Pts',(-3.6224276251006,-4.96189542105038E-11,
5.48850912970297));
#33254=CARTESIAN_POINT('Ctrl Pts',(-3.73518454380962,-4.96189542105038E-11,
5.44464447877917));
#33255=CARTESIAN_POINT('Ctrl Pts',(-3.79238690270398,-4.95907660412871E-11,
5.41288812863561));
#33256=CARTESIAN_POINT('Ctrl Pts',(-3.89031170630778,-4.95907660412871E-11,
5.31852450471732));
#33257=CARTESIAN_POINT('Ctrl Pts',(-3.92692344562731,-4.9585361853769E-11,
5.26626913463268));
#33258=CARTESIAN_POINT('Ctrl Pts',(-3.98096251721357,-4.9585361853769E-11,
5.14916603469699));
#33259=CARTESIAN_POINT('Ctrl Pts',(-3.99724813668202,-4.95755933351878E-11,
5.08357638654045));
#33260=CARTESIAN_POINT('Ctrl Pts',(-3.99989324026065,-4.95755933351878E-11,
5.01155755660981));
#33261=CARTESIAN_POINT('Ctrl Pts',(-4.,-1.30506089359971E-54,5.00577896782872));
#33262=CARTESIAN_POINT('Ctrl Pts',(-4.,-1.30506089359971E-54,5.));
#33263=CARTESIAN_POINT('',(-14.1036297108185,1.72719649817133E-14,22.5));
#33264=CARTESIAN_POINT('Ctrl Pts',(-4.,0.,5.));
#33265=CARTESIAN_POINT('Ctrl Pts',(-4.05262307141051,-0.654498469497874,
5.09114583333333));
#33266=CARTESIAN_POINT('Ctrl Pts',(-3.83031081101585,-2.0164870728516,5.2734375));
#33267=CARTESIAN_POINT('Ctrl Pts',(-2.51852354898032,-3.7208214715467,5.546875));
#33268=CARTESIAN_POINT('Ctrl Pts',(-0.483385262891241,-4.63216118014149,
5.82031249999999));
#33269=CARTESIAN_POINT('Ctrl Pts',(1.8202315402997,-4.46495458019068,6.09375000000001));
#33270=CARTESIAN_POINT('Ctrl Pts',(3.83708110788313,-3.18392684763,6.36718749999999));
#33271=CARTESIAN_POINT('Ctrl Pts',(5.04610371647275,-1.03126017046504,6.640625));
#33272=CARTESIAN_POINT('Ctrl Pts',(5.09366526266359,1.51694087528755,6.9140625));
#33273=CARTESIAN_POINT('Ctrl Pts',(3.89334793428042,3.85517018194508,7.1875));
#33274=CARTESIAN_POINT('Ctrl Pts',(1.66401832874098,5.39254335225655,7.4609375));
#33275=CARTESIAN_POINT('Ctrl Pts',(-1.10655649717025,5.70140348716183,7.73437499999999));
#33276=CARTESIAN_POINT('Ctrl Pts',(-3.76778215269101,4.63360702978987,8.0078125));
#33277=CARTESIAN_POINT('Ctrl Pts',(-5.65899445677288,2.37325046891981,8.28125));
#33278=CARTESIAN_POINT('Ctrl Pts',(-6.27308950292314,-0.59072056165688,
8.5546875));
#33279=CARTESIAN_POINT('Ctrl Pts',(-5.39055984190282,-3.56939135267172,
8.828125));
#33280=CARTESIAN_POINT('Ctrl Pts',(-3.14892433147632,-5.83395881494245,
9.10156249999999));
#33281=CARTESIAN_POINT('Ctrl Pts',(-0.0269941651234124,-6.79383570767807,
9.375));
#33282=CARTESIAN_POINT('Ctrl Pts',(3.25625963494257,-6.14929751664737,9.64843749999999));
#33283=CARTESIAN_POINT('Ctrl Pts',(5.90717602022873,-3.9795144383767,9.921875));
#33284=CARTESIAN_POINT('Ctrl Pts',(7.24915357717334,-0.741104090144106,
10.1953125));
#33285=CARTESIAN_POINT('Ctrl Pts',(6.89437699385751,2.82652617704715,10.46875));
#33286=CARTESIAN_POINT('Ctrl Pts',(4.85214544364602,5.8698051725334,10.7421875));
#33287=CARTESIAN_POINT('Ctrl Pts',(1.54426647303593,7.62518428271038,11.015625));
#33288=CARTESIAN_POINT('Ctrl Pts',(-2.28027404042269,7.61004816114384,11.2890625));
#33289=CARTESIAN_POINT('Ctrl Pts',(-5.71458753487403,5.75276305414747,11.5625));
#33290=CARTESIAN_POINT('Ctrl Pts',(-7.90892381685067,2.42735464211985,11.8359375));
#33291=CARTESIAN_POINT('Ctrl Pts',(-8.280487904502,-1.61956843656331,12.109375));
#33292=CARTESIAN_POINT('Ctrl Pts',(-6.66632390115336,-5.43598980597183,
12.3828125));
#33293=CARTESIAN_POINT('Ctrl Pts',(-3.37955924042675,-8.08843859127204,
12.65625));
#33294=CARTESIAN_POINT('Ctrl Pts',(0.848467586061227,-8.89003850095873,
12.9296875));
#33295=CARTESIAN_POINT('Ctrl Pts',(5.03032510682704,-7.57700176269046,13.203125));
#33296=CARTESIAN_POINT('Ctrl Pts',(8.15306896806033,-4.38851452128152,13.4765625));
#33297=CARTESIAN_POINT('Ctrl Pts',(9.42344702515047,-0.0269941685586242,
13.75));
#33298=CARTESIAN_POINT('Ctrl Pts',(8.46840766181913,4.49584983333495,14.0234375));
#33299=CARTESIAN_POINT('Ctrl Pts',(5.44044821239548,8.09361792642082,14.296875));
#33300=CARTESIAN_POINT('Ctrl Pts',(0.998851072840637,9.86610260310719,14.5703125));
#33301=CARTESIAN_POINT('Ctrl Pts',(-3.83283486415787,9.32382107321317,14.84375));
#33302=CARTESIAN_POINT('Ctrl Pts',(-7.90252221315964,6.52035320687432,15.1171875));
#33303=CARTESIAN_POINT('Ctrl Pts',(-10.2042683613299,2.05727819272983,15.390625));
#33304=CARTESIAN_POINT('Ctrl Pts',(-10.1264293031967,-3.04360991455306,
15.6640625));
#33305=CARTESIAN_POINT('Ctrl Pts',(-7.61217905231046,-7.57400353305939,
15.9375));
#33306=CARTESIAN_POINT('Ctrl Pts',(-3.19069051639217,-10.4253049589896,
16.2109375));
#33307=CARTESIAN_POINT('Ctrl Pts',(2.13258015658974,-10.859571982884,16.484375));
#33308=CARTESIAN_POINT('Ctrl Pts',(7.10419756851087,-8.69904094228735,16.7578125));
#33309=CARTESIAN_POINT('Ctrl Pts',(10.5178826720182,-4.38586792650576,17.03125));
#33310=CARTESIAN_POINT('Ctrl Pts',(11.506987524106,1.10621456668648,17.3046875));
#33311=CARTESIAN_POINT('Ctrl Pts',(9.76344367445795,6.49125888499182,17.578125));
#33312=CARTESIAN_POINT('Ctrl Pts',(5.62810470852332,10.4721791049393,17.8515625));
#33313=CARTESIAN_POINT('Ctrl Pts',(0.0269941874218459,12.0530583592068,
18.125));
#33314=CARTESIAN_POINT('Ctrl Pts',(-5.73544006773032,10.7875177817739,18.3984375));
#33315=CARTESIAN_POINT('Ctrl Pts',(-10.2800597580419,6.90138203286673,18.671875));
#33316=CARTESIAN_POINT('Ctrl Pts',(-12.4830517794477,1.25659796463401,18.9453125));
#33317=CARTESIAN_POINT('Ctrl Pts',(-11.7532648511587,-4.83914337048452,
19.21875));
#33318=CARTESIAN_POINT('Ctrl Pts',(-8.18856157315,-9.93523961480004,19.4921875));
#33319=CARTESIAN_POINT('Ctrl Pts',(-2.57028870635813,-12.7833517182835,
19.765625));
#33320=CARTESIAN_POINT('Ctrl Pts',(3.80694337685198,-12.6428118882295,20.0390625));
#33321=CARTESIAN_POINT('Ctrl Pts',(9.43342435418766,-9.47159216503061,20.3125));
#33322=CARTESIAN_POINT('Ctrl Pts',(12.9416764567355,-3.95403216061098,20.5859375));
#33323=CARTESIAN_POINT('Ctrl Pts',(13.4386753471291,2.64560341469982,20.859375));
#33324=CARTESIAN_POINT('Ctrl Pts',(10.731719416327,8.77238225818101,21.1328125));
#33325=CARTESIAN_POINT('Ctrl Pts',(5.39225375379758,12.9473728958347,21.40625));
#33326=CARTESIAN_POINT('Ctrl Pts',(-1.36411605698682,14.1238442145743,21.6796875));
#33327=CARTESIAN_POINT('Ctrl Pts',(-7.95188025078462,11.9500710288293,21.953125));
#33328=CARTESIAN_POINT('Ctrl Pts',(-12.791953880403,6.86731330268108,22.2265625));
#33329=CARTESIAN_POINT('Ctrl Pts',(-14.0510066394079,2.30770101502388,22.4088541666667));
#33330=CARTESIAN_POINT('Ctrl Pts',(-14.1036297108185,1.72719649817133E-14,
22.5));
#33331=CARTESIAN_POINT('Ctrl Pts',(-14.1036297108185,1.66533453693773E-14,
22.5));
#33332=CARTESIAN_POINT('Ctrl Pts',(-14.1036297108185,1.66533453693773E-14,
22.4931309043374));
#33333=CARTESIAN_POINT('Ctrl Pts',(-14.1034788387995,1.66531662825221E-14,
22.4862623794188));
#33334=CARTESIAN_POINT('Ctrl Pts',(-14.1002811166966,1.66492502023841E-14,
22.4129268800063));
#33335=CARTESIAN_POINT('Ctrl Pts',(-14.0834705379208,1.66292904606448E-14,
22.347144032276));
#33336=CARTESIAN_POINT('Ctrl Pts',(-14.0286766940609,1.65621873551489E-14,
22.2305281202362));
#33337=CARTESIAN_POINT('Ctrl Pts',(-13.9920007099842,1.65187598746323E-14,
22.1787736257353));
#33338=CARTESIAN_POINT('Ctrl Pts',(-13.8942385509797,1.63990357595296E-14,
22.0855877281671));
#33339=CARTESIAN_POINT('Ctrl Pts',(-13.8372385327547,1.65612167903603E-14,
22.0543170879823));
#33340=CARTESIAN_POINT('Ctrl Pts',(-13.7242585716272,1.64228562425978E-14,
22.0110695103706));
#33341=CARTESIAN_POINT('Ctrl Pts',(-13.6586187167909,1.63472900537156E-14,
21.9992928151312));
#33342=CARTESIAN_POINT('Ctrl Pts',(-13.528771486911,1.61882730592651E-14,
22.0011480438118));
#33343=CARTESIAN_POINT('Ctrl Pts',(-13.4663656730128,1.66245598057237E-14,
22.0144829337249));
#33344=CARTESIAN_POINT('Ctrl Pts',(-13.3457270961587,1.64768201587257E-14,
22.0669821183785));
#33345=CARTESIAN_POINT('Ctrl Pts',(-13.2896878319382,1.64156409587601E-14,
22.1059488392955));
#33346=CARTESIAN_POINT('Ctrl Pts',(-13.2067932453118,1.63141243685814E-14,
22.1911381458157));
#33347=CARTESIAN_POINT('Ctrl Pts',(-13.168924538057,1.55630875029458E-14,
22.2410844954725));
#33348=CARTESIAN_POINT('Ctrl Pts',(-13.1164702794208,1.54988495630052E-14,
22.3673474980845));
#33349=CARTESIAN_POINT('Ctrl Pts',(-13.1039637101555,1.54821629830264E-14,
22.4337645256774));
#33350=CARTESIAN_POINT('Ctrl Pts',(-13.1042036570148,1.54824568331797E-14,
22.5666921253015));
#33351=CARTESIAN_POINT('Ctrl Pts',(-13.1171254904007,1.54984491412652E-14,
22.6335431762745));
#33352=CARTESIAN_POINT('Ctrl Pts',(-13.1707730203801,1.55641484171366E-14,
22.7613131645324));
#33353=CARTESIAN_POINT('Ctrl Pts',(-13.2095003145773,1.6725202005197E-14,
22.8116763951221));
#33354=CARTESIAN_POINT('Ctrl Pts',(-13.2928111432349,1.68272283448469E-14,
22.896640266457));
#33355=CARTESIAN_POINT('Ctrl Pts',(-13.3492037310432,1.69009548416532E-14,
22.9355463321452));
#33356=CARTESIAN_POINT('Ctrl Pts',(-13.4652439179706,1.70430630851463E-14,
22.9850914692808));
#33357=CARTESIAN_POINT('Ctrl Pts',(-13.5262140083287,1.55816880134289E-14,
22.999714984015));
#33358=CARTESIAN_POINT('Ctrl Pts',(-13.6607096755624,1.57463977018059E-14,
23.0007059664907));
#33359=CARTESIAN_POINT('Ctrl Pts',(-13.7260573365682,1.58201349665679E-14,
22.9885091295348));
#33360=CARTESIAN_POINT('Ctrl Pts',(-13.8388142552453,1.59582223661075E-14,
22.9446444784495));
#33361=CARTESIAN_POINT('Ctrl Pts',(-13.8960166140677,1.66282530092132E-14,
22.9128881282363));
#33362=CARTESIAN_POINT('Ctrl Pts',(-13.9939414175529,1.67481763063585E-14,
22.8185245041776));
#33363=CARTESIAN_POINT('Ctrl Pts',(-14.0305531568207,1.67881918203982E-14,
22.7662691340177));
#33364=CARTESIAN_POINT('Ctrl Pts',(-14.0845922282433,1.68543705962449E-14,
22.649166033998));
#33365=CARTESIAN_POINT('Ctrl Pts',(-14.1008778476158,1.68694037472559E-14,
22.5835763858428));
#33366=CARTESIAN_POINT('Ctrl Pts',(-14.1035229510752,1.68726430647407E-14,
22.5115575563802));
#33367=CARTESIAN_POINT('Ctrl Pts',(-14.1036297108185,1.68723542082194E-14,
22.5057789677136));
#33368=CARTESIAN_POINT('Ctrl Pts',(-14.1036297108185,1.68723542082194E-14,
22.5));
#33369=CARTESIAN_POINT('Origin',(-13.6036297108184,1.66596415821396E-14,
22.5));
#33370=CARTESIAN_POINT('Origin',(-3.5,0.,5.));
#33465=UNCERTAINTY_MEASURE_WITH_UNIT(LENGTH_MEASURE(0.01),#33475,
'DISTANCE_ACCURACY_VALUE',
'Maximum model space distance between geometric entities at asserted c
onnectivities');
#33467=UNCERTAINTY_MEASURE_WITH_UNIT(LENGTH_MEASURE(0.01),#33475,
'DISTANCE_ACCURACY_VALUE',
'Maximum model space distance between geometric entities at asserted c
onnectivities');
#33472=(
GEOMETRIC_REPRESENTATION_CONTEXT(3)
GLOBAL_UNCERTAINTY_ASSIGNED_CONTEXT((#33465))
GLOBAL_UNIT_ASSIGNED_CONTEXT((#33475,#33477,#33478))
REPRESENTATION_CONTEXT('','3D')
);
#33474=(
GEOMETRIC_REPRESENTATION_CONTEXT(3)
GLOBAL_UNCERTAINTY_ASSIGNED_CONTEXT((#33467))
GLOBAL_UNIT_ASSIGNED_CONTEXT((#33475,#33477,#33478))
REPRESENTATION_CONTEXT('','3D')
);
#33475=(
LENGTH_UNIT()
NAMED_UNIT(*)
SI_UNIT(.MILLI.,.METRE.)
);
#33477=(
NAMED_UNIT(*)
PLANE_ANGLE_UNIT()
SI_UNIT($,.RADIAN.)
);
#33478=(
NAMED_UNIT(*)
SI_UNIT($,.STERADIAN.)
SOLID_ANGLE_UNIT()
);
#33483=SHAPE_DEFINITION_REPRESENTATION(#33489,#33500);
#33489=PRODUCT_DEFINITION_SHAPE('',$,#33507);
#33500=SHAPE_REPRESENTATION('',(#3125),#33472);
#33502=PRODUCT_DEFINITION_CONTEXT('part definition',#33522,'design');
#33507=PRODUCT_DEFINITION('Spring','Spring',#33513,#33502);
#33513=PRODUCT_DEFINITION_FORMATION('',$,#33528);
#33522=APPLICATION_CONTEXT(
'Core Data for Automotive Mechanical Design Process');
#33523=PRODUCT_CONTEXT('part definition',#33522,'mechanical');
#33528=PRODUCT('Spring','Spring',$,(#33523));
#33531=PRESENTATION_STYLE_ASSIGNMENT((#33533));
#33533=SURFACE_STYLE_USAGE(.BOTH.,#33535);
#33535=SURFACE_SIDE_STYLE('',(#33537));
#33537=SURFACE_STYLE_FILL_AREA(#33539);
#33539=FILL_AREA_STYLE('Opaque(203,203,203)',(#33541));
#33541=FILL_AREA_STYLE_COLOUR('Opaque(203,203,203)',#33543);
#33543=COLOUR_RGB('Opaque(203,203,203)', 0.09019608, 0.27058824, 0.51372549);
ENDSEC;
END-ISO-10303-21;
